ISO-10303-21;
HEADER;
FILE_DESCRIPTION (('STEP AP214'),
    '1' );
FILE_NAME ('Input Shaft.step',
    '2026-10-08T09:53:37',
    ( '' ),
    ( '' ),
    'SwSTEP 2.0',
    'SolidWorks 2026',
    '' );
FILE_SCHEMA (( 'AUTOMOTIVE_DESIGN' ));
ENDSEC;

DATA;
#120=CIRCLE ( 'NONE', #42098, 12.49999999999999645 ) ;
#138=AXIS2_PLACEMENT_3D ( 'NONE', #23331, #68076, #16566 ) ;
#203=PRESENTATION_STYLE_ASSIGNMENT (( #57300 ) ) ;
#393=DIRECTION ( 'NONE',  ( 0.000000000000000000, 0.000000000000000000, 1.000000000000000000 ) ) ;
#440=LINE ( 'NONE', #70277, #63595 ) ;
#521=FACE_OUTER_BOUND ( 'NONE', #2721, .T. ) ;
#576=ORIENTED_EDGE ( 'NONE', *, *, #2147, .F. ) ;
#579=VECTOR ( 'NONE', #18980, 1000.000000000000000 ) ;
#652=CIRCLE ( 'NONE', #28184, 11.59999999999999787 ) ;
#718=EDGE_CURVE ( 'NONE', #14320, #31534, #29205, .T. ) ;
#771=CARTESIAN_POINT ( 'NONE',  ( 0.000000000000000000, 0.000000000000000000, 42.00000000000001421 ) ) ;
#870=VECTOR ( 'NONE', #36288, 1000.000000000000000 ) ;
#872=ORIENTED_EDGE ( 'NONE', *, *, #54865, .T. ) ;
#927=CYLINDRICAL_SURFACE ( 'NONE', #15144, 12.49999999999999645 ) ;
#939=ORIENTED_EDGE ( 'NONE', *, *, #65612, .F. ) ;
#955=ORIENTED_EDGE ( 'NONE', *, *, #71022, .T. ) ;
#986=VERTEX_POINT ( 'NONE', #10495 ) ;
#1068=DIRECTION ( 'NONE',  ( 0.000000000000000000, 0.000000000000000000, 1.000000000000000000 ) ) ;
#1108=ORIENTED_EDGE ( 'NONE', *, *, #8076, .F. ) ;
#1206=CARTESIAN_POINT ( 'NONE',  ( -9.937067298023309903, 7.583184918921312523, 52.00000000000002132 ) ) ;
#1281=VERTEX_POINT ( 'NONE', #37144 ) ;
#1290=CYLINDRICAL_SURFACE ( 'NONE', #1954, 12.49999999999999645 ) ;
#1364=PLANE ( 'NONE',  #1524 ) ;
#1384=CARTESIAN_POINT ( 'NONE',  ( -6.170112525937322623, 10.87104923258428180, 125.0000000000000000 ) ) ;
#1500=CARTESIAN_POINT ( 'NONE',  ( 0.000000000000000000, 0.000000000000000000, 53.20000000000001705 ) ) ;
#1524=AXIS2_PLACEMENT_3D ( 'NONE', #17861, #63742, #12218 ) ;
#1607=DIRECTION ( 'NONE',  ( 0.000000000000000000, 0.000000000000000000, -1.000000000000000000 ) ) ;
#1758=LINE ( 'NONE', #18263, #66097 ) ;
#1764=EDGE_CURVE ( 'NONE', #39181, #43104, #22066, .T. ) ;
#1779=CIRCLE ( 'NONE', #46184, 12.49999999999999645 ) ;
#1809=VERTEX_POINT ( 'NONE', #69229 ) ;
#1954=AXIS2_PLACEMENT_3D ( 'NONE', #53481, #47472, #13254 ) ;
#1974=VERTEX_POINT ( 'NONE', #19559 ) ;
#1983=CARTESIAN_POINT ( 'NONE',  ( 12.49999999999999645, 1.530808498934191127E-15, -125.0000000000000000 ) ) ;
#2123=VECTOR ( 'NONE', #44670, 1000.000000000000000 ) ;
#2147=EDGE_CURVE ( 'NONE', #16094, #45782, #53018, .T. ) ;
#2193=ADVANCED_FACE ( 'NONE', ( #15396 ), #3050, .T. ) ;
#2211=AXIS2_PLACEMENT_3D ( 'NONE', #12517, #45652, #69669 ) ;
#2214=DIRECTION ( 'NONE',  ( 1.000000000000000000, 0.000000000000000000, 0.000000000000000000 ) ) ;
#2244=DIRECTION ( 'NONE',  ( 1.000000000000000000, 0.000000000000000000, -0.000000000000000000 ) ) ;
#2275=VERTEX_POINT ( 'NONE', #16151 ) ;
#2354=CIRCLE ( 'NONE', #59913, 12.49999999999999645 ) ;
#2425=ORIENTED_EDGE ( 'NONE', *, *, #21212, .T. ) ;
#2439=ORIENTED_EDGE ( 'NONE', *, *, #42439, .T. ) ;
#2501=DIRECTION ( 'NONE',  ( 1.000000000000000000, 0.000000000000000000, 0.000000000000000000 ) ) ;
#2592=CARTESIAN_POINT ( 'NONE',  ( -6.170112525937308412, 10.87104923258428890, 52.00000000000002132 ) ) ;
#2611=DIRECTION ( 'NONE',  ( 0.6575728627325955200, -0.7533909544171997208, 0.000000000000000000 ) ) ;
#2721=EDGE_LOOP ( 'NONE', ( #34967, #21826, #70511, #58260 ) ) ;
#2812=FACE_OUTER_BOUND ( 'NONE', #64835, .T. ) ;
#2855=LINE ( 'NONE', #8832, #70358 ) ;
#2882=EDGE_CURVE ( 'NONE', #54619, #42737, #31756, .T. ) ;
#3050=CYLINDRICAL_SURFACE ( 'NONE', #62644, 11.59999999999999787 ) ;
#3066=ORIENTED_EDGE ( 'NONE', *, *, #4965, .T. ) ;
#3118=EDGE_CURVE ( 'NONE', #1974, #40171, #7423, .T. ) ;
#3157=VECTOR ( 'NONE', #57271, 1000.000000000000000 ) ;
#3160=LINE ( 'NONE', #28270, #49031 ) ;
#3181=VERTEX_POINT ( 'NONE', #64943 ) ;
#3228=( NAMED_UNIT ( * ) PLANE_ANGLE_UNIT ( ) SI_UNIT ( $, .RADIAN. ) );
#3230=DIRECTION ( 'NONE',  ( 0.000000000000000000, 0.000000000000000000, 1.000000000000000000 ) ) ;
#3255=CARTESIAN_POINT ( 'NONE',  ( 0.000000000000000000, 0.000000000000000000, 125.0000000000000000 ) ) ;
#3299=DIRECTION ( 'NONE',  ( 0.000000000000000000, 0.000000000000000000, 1.000000000000000000 ) ) ;
#3307=CARTESIAN_POINT ( 'NONE',  ( 0.000000000000000000, 0.000000000000000000, -54.99999999999998579 ) ) ;
#3438=VERTEX_POINT ( 'NONE', #10001 ) ;
#3575=CARTESIAN_POINT ( 'NONE',  ( 0.000000000000000000, 0.000000000000000000, -43.79999999999998295 ) ) ;
#3653=AXIS2_PLACEMENT_3D ( 'NONE', #56460, #12425, #69210 ) ;
#3711=PLANE ( 'NONE',  #34380 ) ;
#3815=ORIENTED_EDGE ( 'NONE', *, *, #24842, .F. ) ;
#3937=LINE ( 'NONE', #45262, #14568 ) ;
#3946=DIRECTION ( 'NONE',  ( -0.000000000000000000, -0.000000000000000000, -1.000000000000000000 ) ) ;
#4079=DIRECTION ( 'NONE',  ( 0.6575728627325955200, -0.7533909544171997208, 0.000000000000000000 ) ) ;
#4187=ORIENTED_EDGE ( 'NONE', *, *, #30719, .T. ) ;
#4223=CARTESIAN_POINT ( 'NONE',  ( 0.000000000000000000, 0.000000000000000000, -54.99999999999998579 ) ) ;
#4301=ADVANCED_FACE ( 'NONE', ( #55318 ), #62084, .T. ) ;
#4372=DIRECTION ( 'NONE',  ( -0.7533909544171996098, -0.6575728627325955200, 7.625282249115660656E-32 ) ) ;
#4416=PLANE ( 'NONE',  #70025 ) ;
#4514=FACE_OUTER_BOUND ( 'NONE', #12098, .T. ) ;
#4531=CARTESIAN_POINT ( 'NONE',  ( -12.49999999999999645, 0.000000000000000000, 53.20000000000001705 ) ) ;
#4535=CARTESIAN_POINT ( 'NONE',  ( 0.000000000000000000, 0.000000000000000000, 42.00000000000001421 ) ) ;
#4658=CARTESIAN_POINT ( 'NONE',  ( 0.000000000000000000, 0.000000000000000000, 125.0000000000000000 ) ) ;
#4771=ORIENTED_EDGE ( 'NONE', *, *, #69406, .T. ) ;
#4813=ORIENTED_EDGE ( 'NONE', *, *, #52101, .F. ) ;
#4965=EDGE_CURVE ( 'NONE', #27241, #65977, #17086, .T. ) ;
#5043=DIRECTION ( 'NONE',  ( 8.090853898039833646E-17, -9.269810975720164453E-17, 1.000000000000000000 ) ) ;
#5055=ADVANCED_FACE ( 'NONE', ( #25739, #66350 ), #9186, .F. ) ;
#5207=FACE_OUTER_BOUND ( 'NONE', #24415, .T. ) ;
#5213=FACE_BOUND ( 'NONE', #20889, .T. ) ;
#5261=AXIS2_PLACEMENT_3D ( 'NONE', #15296, #53673, #2214 ) ;
#5288=AXIS2_PLACEMENT_3D ( 'NONE', #44072, #66991, #33144 ) ;
#5346=DIRECTION ( 'NONE',  ( 1.000000000000000000, 0.000000000000000000, -0.000000000000000000 ) ) ;
#5403=FACE_OUTER_BOUND ( 'NONE', #35707, .T. ) ;
#5444=SURFACE_STYLE_FILL_AREA ( #16331 ) ;
#5615=CARTESIAN_POINT ( 'NONE',  ( -12.49999999999999645, 0.000000000000000000, 125.0000000000000000 ) ) ;
#5740=VERTEX_POINT ( 'NONE', #1206 ) ;
#6067=DIRECTION ( 'NONE',  ( 0.000000000000000000, 0.000000000000000000, 1.000000000000000000 ) ) ;
#6073=CIRCLE ( 'NONE', #15662, 11.59999999999999787 ) ;
#6138=CARTESIAN_POINT ( 'NONE',  ( 0.000000000000000000, 0.000000000000000000, 125.0000000000000000 ) ) ;
#6318=DIRECTION ( 'NONE',  ( 0.000000000000000000, 0.000000000000000000, 1.000000000000000000 ) ) ;
#6615=ADVANCED_FACE ( 'NONE', ( #55158 ), #4416, .F. ) ;
#6618=CARTESIAN_POINT ( 'NONE',  ( -7.469491406282116053, 4.756046723998915482, -45.00000000000000000 ) ) ;
#6630=CARTESIAN_POINT ( 'NONE',  ( 0.000000000000000000, 0.000000000000000000, -43.79999999999998295 ) ) ;
#6660=DIRECTION ( 'NONE',  ( -0.000000000000000000, -0.000000000000000000, -1.000000000000000000 ) ) ;
#6784=PRODUCT_DEFINITION ( 'UNKNOWN', '', #32838, #71699 ) ;
#6834=CARTESIAN_POINT ( 'NONE',  ( 12.49999999999999645, 1.530808498934191127E-15, 53.20000000000001705 ) ) ;
#6857=FACE_OUTER_BOUND ( 'NONE', #28370, .T. ) ;
#6877=CARTESIAN_POINT ( 'NONE',  ( 12.49999999999999645, 1.530808498934191127E-15, 125.0000000000000000 ) ) ;
#6926=CARTESIAN_POINT ( 'NONE',  ( -9.937067298023318784, 7.583184918921300088, 125.0000000000000000 ) ) ;
#6964=AXIS2_PLACEMENT_3D ( 'NONE', #16438, #15702, #45025 ) ;
#7127=AXIS2_PLACEMENT_3D ( 'NONE', #39842, #393, #11608 ) ;
#7192=FACE_OUTER_BOUND ( 'NONE', #30183, .T. ) ;
#7273=CARTESIAN_POINT ( 'NONE',  ( -12.49999999999999645, 0.000000000000000000, 125.0000000000000000 ) ) ;
#7331=EDGE_CURVE ( 'NONE', #58186, #73677, #73621, .T. ) ;
#7332=ORIENTED_EDGE ( 'NONE', *, *, #36488, .T. ) ;
#7363=CARTESIAN_POINT ( 'NONE',  ( 0.000000000000000000, 0.000000000000000000, 42.00000000000001421 ) ) ;
#7423=LINE ( 'NONE', #29224, #30936 ) ;
#7430=LINE ( 'NONE', #70185, #35120 ) ;
#7529=DIRECTION ( 'NONE',  ( 1.000000000000000000, 0.000000000000000000, 0.000000000000000000 ) ) ;
#7618=VERTEX_POINT ( 'NONE', #9276 ) ;
#7687=CARTESIAN_POINT ( 'NONE',  ( 0.000000000000000000, 0.000000000000000000, 42.00000000000001421 ) ) ;
#7697=DIRECTION ( 'NONE',  ( -1.000000000000000000, 0.000000000000000000, 0.000000000000000000 ) ) ;
#7701=ADVANCED_BREP_SHAPE_REPRESENTATION ( '', ( #36653, #43395 ), #21791 ) ;
#7808=CARTESIAN_POINT ( 'NONE',  ( 11.59999999999999787, 1.420590287010929336E-15, 53.20000000000001705 ) ) ;
#7830=CARTESIAN_POINT ( 'NONE',  ( -6.170112525937308412, 10.87104923258428890, 42.00000000000001421 ) ) ;
#7861=DIRECTION ( 'NONE',  ( 0.000000000000000000, 0.000000000000000000, -1.000000000000000000 ) ) ;
#7902=EDGE_CURVE ( 'NONE', #26184, #70313, #29154, .T. ) ;
#7926=CARTESIAN_POINT ( 'NONE',  ( -12.40464318976452596, 10.41032311384371489, 52.00000000000002132 ) ) ;
#7964=VECTOR ( 'NONE', #4372, 1000.000000000000114 ) ;
#8076=EDGE_CURVE ( 'NONE', #3438, #39181, #72131, .T. ) ;
#8083=DIRECTION ( 'NONE',  ( 0.000000000000000000, 0.000000000000000000, 1.000000000000000000 ) ) ;
#8166=CIRCLE ( 'NONE', #9338, 12.49999999999999645 ) ;
#8417=CARTESIAN_POINT ( 'NONE',  ( -12.40464318976452596, 10.41032311384371489, 32.98187577049606745 ) ) ;
#8425=EDGE_LOOP ( 'NONE', ( #34483, #3066 ) ) ;
#8504=FACE_OUTER_BOUND ( 'NONE', #17303, .T. ) ;
#8524=SHAPE_REPRESENTATION ( 'Input Shaft', ( #43395 ), #21791 ) ;
#8539=ORIENTED_EDGE ( 'NONE', *, *, #13179, .F. ) ;
#8595=ORIENTED_EDGE ( 'NONE', *, *, #25652, .F. ) ;
#8613=ORIENTED_EDGE ( 'NONE', *, *, #65612, .T. ) ;
#8732=AXIS2_PLACEMENT_3D ( 'NONE', #12791, #19906, #52652 ) ;
#8781=PLANE ( 'NONE',  #47939 ) ;
#8807=ORIENTED_EDGE ( 'NONE', *, *, #15284, .T. ) ;
#8825=DIRECTION ( 'NONE',  ( 1.000000000000000000, 0.000000000000000000, 0.000000000000000000 ) ) ;
#8832=CARTESIAN_POINT ( 'NONE',  ( -3.702536634196095910, 8.043911037661889196, 32.98187577049606745 ) ) ;
#8889=LINE ( 'NONE', #42734, #72255 ) ;
#8903=CARTESIAN_POINT ( 'NONE',  ( 0.000000000000000000, 0.000000000000000000, 42.00000000000001421 ) ) ;
#9061=ORIENTED_EDGE ( 'NONE', *, *, #60701, .F. ) ;
#9186=PLANE ( 'NONE',  #39101 ) ;
#9210=ORIENTED_EDGE ( 'NONE', *, *, #49703, .T. ) ;
#9255=ORIENTED_EDGE ( 'NONE', *, *, #11301, .F. ) ;
#9258=ORIENTED_EDGE ( 'NONE', *, *, #52101, .T. ) ;
#9276=CARTESIAN_POINT ( 'NONE',  ( -3.702536634196095910, 8.043911037661889196, 42.00000000000001421 ) ) ;
#9319=EDGE_CURVE ( 'NONE', #43104, #63923, #1758, .T. ) ;
#9338=AXIS2_PLACEMENT_3D ( 'NONE', #46602, #63908, #12378 ) ;
#9347=EDGE_CURVE ( 'NONE', #47656, #61855, #120, .T. ) ;
#9456=FACE_OUTER_BOUND ( 'NONE', #62134, .T. ) ;
#9488=EDGE_LOOP ( 'NONE', ( #45822, #7332, #68645, #66316, #47086, #10653 ) ) ;
#9600=DIRECTION ( 'NONE',  ( 1.000000000000000000, 0.000000000000000000, 0.000000000000000000 ) ) ;
#9729=ORIENTED_EDGE ( 'NONE', *, *, #15091, .F. ) ;
#9913=DIRECTION ( 'NONE',  ( 0.7533909544171996098, 0.6575728627325955200, -7.625282249115660656E-32 ) ) ;
#9915=DIRECTION ( 'NONE',  ( -0.6575728627325957421, 0.7533909544171993877, 1.230411769795008318E-16 ) ) ;
#9986=CARTESIAN_POINT ( 'NONE',  ( -12.49999999999999645, 0.000000000000000000, -125.0000000000000000 ) ) ;
#10001=CARTESIAN_POINT ( 'NONE',  ( -9.332068499558253905, 6.890028847512361665, -54.99999999999998579 ) ) ;
#10008=DIRECTION ( 'NONE',  ( 0.000000000000000000, 0.000000000000000000, 1.000000000000000000 ) ) ;
#10071=CARTESIAN_POINT ( 'NONE',  ( 11.59999999999999787, 1.420590287010929336E-15, -43.79999999999998295 ) ) ;
#10263=ORIENTED_EDGE ( 'NONE', *, *, #43882, .T. ) ;
#10290=AXIS2_PLACEMENT_3D ( 'NONE', #71205, #37403, #60334 ) ;
#10335=EDGE_CURVE ( 'NONE', #32157, #3438, #440, .T. ) ;
#10417=CARTESIAN_POINT ( 'NONE',  ( 0.000000000000000000, 0.000000000000000000, -125.0000000000000000 ) ) ;
#10423=PLANE ( 'NONE',  #6964 ) ;
#10482=AXIS2_PLACEMENT_3D ( 'NONE', #63554, #58269, #28953 ) ;
#10495=CARTESIAN_POINT ( 'NONE',  ( 12.49999999999999645, 1.530808498934191127E-15, -43.79999999999998295 ) ) ;
#10531=FACE_BOUND ( 'NONE', #73356, .T. ) ;
#10534=DIRECTION ( 'NONE',  ( 0.000000000000000000, 0.000000000000000000, 1.000000000000000000 ) ) ;
#10547=EDGE_LOOP ( 'NONE', ( #4813, #16224, #64213, #56670 ) ) ;
#10563=CARTESIAN_POINT ( 'NONE',  ( 11.59999999999999787, 1.420590287010929336E-15, -43.79999999999998295 ) ) ;
#10583=CARTESIAN_POINT ( 'NONE',  ( 0.000000000000000000, 0.000000000000000000, 52.00000000000002132 ) ) ;
#10632=VECTOR ( 'NONE', #29437, 1000.000000000000000 ) ;
#10653=ORIENTED_EDGE ( 'NONE', *, *, #66791, .F. ) ;
#10774=AXIS2_PLACEMENT_3D ( 'NONE', #43133, #71672, #66067 ) ;
#10807=EDGE_CURVE ( 'NONE', #68344, #63923, #55191, .T. ) ;
#11003=EDGE_CURVE ( 'NONE', #72303, #50389, #51598, .T. ) ;
#11084=ORIENTED_EDGE ( 'NONE', *, *, #38618, .T. ) ;
#11172=FACE_BOUND ( 'NONE', #47297, .T. ) ;
#11301=EDGE_CURVE ( 'NONE', #37316, #1281, #12238, .T. ) ;
#11336=CARTESIAN_POINT ( 'NONE',  ( -12.40464318976452596, 10.41032311384371489, 52.00000000000002132 ) ) ;
#11482=ORIENTED_EDGE ( 'NONE', *, *, #36488, .F. ) ;
#11602=DIRECTION ( 'NONE',  ( -0.000000000000000000, -0.000000000000000000, -1.000000000000000000 ) ) ;
#11605=ADVANCED_FACE ( 'NONE', ( #67728 ), #16216, .T. ) ;
#11608=DIRECTION ( 'NONE',  ( 1.000000000000000000, 0.000000000000000000, 0.000000000000000000 ) ) ;
#11685=DIRECTION ( 'NONE',  ( 0.7533909544171997208, 0.6575728627325956310, -6.162975822039155825E-32 ) ) ;
#11716=EDGE_CURVE ( 'NONE', #12834, #29431, #14504, .T. ) ;
#11776=CARTESIAN_POINT ( 'NONE',  ( 0.000000000000000000, 0.000000000000000000, 52.00000000000002132 ) ) ;
#11790=LINE ( 'NONE', #51663, #66522 ) ;
#11830=VECTOR ( 'NONE', #1607, 1000.000000000000000 ) ;
#12012=ORIENTED_EDGE ( 'NONE', *, *, #12716, .T. ) ;
#12098=EDGE_LOOP ( 'NONE', ( #38294, #64366 ) ) ;
#12218=DIRECTION ( 'NONE',  ( 0.7533909544171998318, 0.6575728627325954090, 0.000000000000000000 ) ) ;
#12238=LINE ( 'NONE', #54235, #50467 ) ;
#12245=CARTESIAN_POINT ( 'NONE',  ( 0.000000000000000000, 0.000000000000000000, -43.79999999999998295 ) ) ;
#12246=EDGE_CURVE ( 'NONE', #48900, #58054, #72915, .T. ) ;
#12249=CIRCLE ( 'NONE', #73471, 12.49999999999999645 ) ;
#12272=CARTESIAN_POINT ( 'NONE',  ( 0.000000000000000000, 0.000000000000000000, -54.99999999999998579 ) ) ;
#12302=EDGE_LOOP ( 'NONE', ( #47372, #39568, #73380, #55596 ) ) ;
#12310=ORIENTED_EDGE ( 'NONE', *, *, #10335, .T. ) ;
#12322=DIRECTION ( 'NONE',  ( 0.000000000000000000, 0.000000000000000000, 1.000000000000000000 ) ) ;
#12369=PLANE ( 'NONE',  #18546 ) ;
#12378=DIRECTION ( 'NONE',  ( 1.000000000000000000, 0.000000000000000000, 0.000000000000000000 ) ) ;
#12381=DIRECTION ( 'NONE',  ( 0.000000000000000000, 0.000000000000000000, 1.000000000000000000 ) ) ;
#12425=DIRECTION ( 'NONE',  ( -0.000000000000000000, -0.000000000000000000, -1.000000000000000000 ) ) ;
#12427=DIRECTION ( 'NONE',  ( -1.000000000000000000, 0.000000000000000000, 0.000000000000000000 ) ) ;
#12445=FILL_AREA_STYLE ('',( #23732 ) ) ;
#12491=CARTESIAN_POINT ( 'NONE',  ( 0.000000000000000000, 0.000000000000000000, -125.0000000000000000 ) ) ;
#12517=CARTESIAN_POINT ( 'NONE',  ( 0.000000000000000000, 0.000000000000000000, 40.80000000000001847 ) ) ;
#12716=EDGE_CURVE ( 'NONE', #1281, #3181, #30962, .T. ) ;
#12723=CARTESIAN_POINT ( 'NONE',  ( -9.937067298023309903, 7.583184918921312523, 42.00000000000001421 ) ) ;
#12791=CARTESIAN_POINT ( 'NONE',  ( 6.782329983125267248, 10.49999999999999645, -105.0000000000000000 ) ) ;
#12812=CARTESIAN_POINT ( 'NONE',  ( -9.332068499558246799, 6.890028847512375876, 42.00000000000001421 ) ) ;
#12834=VERTEX_POINT ( 'NONE', #65163 ) ;
#12890=EDGE_CURVE ( 'NONE', #39717, #58054, #24198, .T. ) ;
#12975=DIRECTION ( 'NONE',  ( 0.000000000000000000, 0.000000000000000000, 1.000000000000000000 ) ) ;
#13141=DIRECTION ( 'NONE',  ( 1.000000000000000000, 0.000000000000000000, 0.000000000000000000 ) ) ;
#13179=EDGE_CURVE ( 'NONE', #986, #16639, #40646, .T. ) ;
#13191=SURFACE_STYLE_USAGE ( .BOTH. , #28999 ) ;
#13193=DIRECTION ( 'NONE',  ( 0.000000000000000000, 0.000000000000000000, -1.000000000000000000 ) ) ;
#13244=ORIENTED_EDGE ( 'NONE', *, *, #49197, .T. ) ;
#13254=DIRECTION ( 'NONE',  ( -1.000000000000000000, 0.000000000000000000, 0.000000000000000000 ) ) ;
#13305=ORIENTED_EDGE ( 'NONE', *, *, #49197, .F. ) ;
#13510=ORIENTED_EDGE ( 'NONE', *, *, #25557, .F. ) ;
#13547=LINE ( 'NONE', #19917, #40699 ) ;
#13644=ADVANCED_FACE ( 'NONE', ( #30955 ), #8781, .F. ) ;
#13687=DIRECTION ( 'NONE',  ( 1.000000000000000000, 0.000000000000000000, 0.000000000000000000 ) ) ;
#13809=DIRECTION ( 'NONE',  ( 0.000000000000000000, 0.000000000000000000, -1.000000000000000000 ) ) ;
#14140=CARTESIAN_POINT ( 'NONE',  ( 12.49999999999999645, 1.530808498934191127E-15, 125.0000000000000000 ) ) ;
#14306=DIRECTION ( 'NONE',  ( 0.6575728627325957421, -0.7533909544171994987, 0.000000000000000000 ) ) ;
#14320=VERTEX_POINT ( 'NONE', #38756 ) ;
#14410=EDGE_CURVE ( 'NONE', #43104, #35072, #33266, .T. ) ;
#14416=EDGE_LOOP ( 'NONE', ( #50515, #58161, #49177, #48301 ) ) ;
#14423=DIRECTION ( 'NONE',  ( -8.090853898039828715E-17, 9.269810975720166919E-17, -1.000000000000000000 ) ) ;
#14504=CIRCLE ( 'NONE', #61323, 11.59999999999999787 ) ;
#14520=ORIENTED_EDGE ( 'NONE', *, *, #52609, .F. ) ;
#14555=DIRECTION ( 'NONE',  ( 1.000000000000000000, 0.000000000000000000, 0.000000000000000000 ) ) ;
#14568=VECTOR ( 'NONE', #67437, 1000.000000000000000 ) ;
#14664=AXIS2_PLACEMENT_3D ( 'NONE', #8903, #10008, #21271 ) ;
#14782=DIRECTION ( 'NONE',  ( -0.7533909544171996098, -0.6575728627325956310, 0.000000000000000000 ) ) ;
#14860=VECTOR ( 'NONE', #68750, 1000.000000000000000 ) ;
#14934=DIRECTION ( 'NONE',  ( 1.000000000000000000, 0.000000000000000000, -0.000000000000000000 ) ) ;
#14946=EDGE_CURVE ( 'NONE', #50389, #72303, #69879, .T. ) ;
#15006=EDGE_CURVE ( 'NONE', #32157, #33300, #7430, .T. ) ;
#15036=CARTESIAN_POINT ( 'NONE',  ( 0.000000000000000000, 0.000000000000000000, -44.99999999999998579 ) ) ;
#15041=VECTOR ( 'NONE', #62674, 1000.000000000000000 ) ;
#15091=EDGE_CURVE ( 'NONE', #36680, #65205, #60361, .T. ) ;
#15144=AXIS2_PLACEMENT_3D ( 'NONE', #63312, #52762, #46019 ) ;
#15284=EDGE_CURVE ( 'NONE', #57864, #73677, #31566, .T. ) ;
#15296=CARTESIAN_POINT ( 'NONE',  ( 0.000000000000000000, 0.000000000000000000, -44.99999999999998579 ) ) ;
#15368=ORIENTED_EDGE ( 'NONE', *, *, #62559, .F. ) ;
#15396=FACE_OUTER_BOUND ( 'NONE', #60504, .T. ) ;
#15532=ADVANCED_FACE ( 'NONE', ( #22466 ), #22845, .T. ) ;
#15590=( NAMED_UNIT ( * ) SI_UNIT ( $, .STERADIAN. ) SOLID_ANGLE_UNIT ( ) );
#15662=AXIS2_PLACEMENT_3D ( 'NONE', #19520, #29682, #13141 ) ;
#15683=DIRECTION ( 'NONE',  ( 0.000000000000000000, 0.000000000000000000, 1.000000000000000000 ) ) ;
#15702=DIRECTION ( 'NONE',  ( 0.000000000000000000, 0.000000000000000000, 1.000000000000000000 ) ) ;
#15808=ADVANCED_FACE ( 'NONE', ( #8504 ), #48715, .T. ) ;
#15847=DIRECTION ( 'NONE',  ( -1.000000000000000000, 0.000000000000000000, 0.000000000000000000 ) ) ;
#15875=DIRECTION ( 'NONE',  ( 0.000000000000000000, 0.000000000000000000, 1.000000000000000000 ) ) ;
#16094=VERTEX_POINT ( 'NONE', #6834 ) ;
#16129=CARTESIAN_POINT ( 'NONE',  ( 11.59999999999999787, 1.420590287010929336E-15, -44.99999999999998579 ) ) ;
#16151=CARTESIAN_POINT ( 'NONE',  ( 12.49999999999999645, 1.530808498934191127E-15, -54.99999999999998579 ) ) ;
#16179=ORIENTED_EDGE ( 'NONE', *, *, #68502, .F. ) ;
#16216=CYLINDRICAL_SURFACE ( 'NONE', #3653, 12.49999999999999645 ) ;
#16224=ORIENTED_EDGE ( 'NONE', *, *, #17007, .F. ) ;
#16248=CIRCLE ( 'NONE', #43849, 11.59999999999999787 ) ;
#16331=FILL_AREA_STYLE ('',( #25758 ) ) ;
#16438=CARTESIAN_POINT ( 'NONE',  ( 0.000000000000000000, 0.000000000000000000, 53.20000000000001705 ) ) ;
#16465=DIRECTION ( 'NONE',  ( 8.090853898039833646E-17, -9.269810975720164453E-17, 1.000000000000000000 ) ) ;
#16566=DIRECTION ( 'NONE',  ( 1.000000000000000000, 0.000000000000000000, 0.000000000000000000 ) ) ;
#16625=VECTOR ( 'NONE', #55635, 1000.000000000000114 ) ;
#16639=VERTEX_POINT ( 'NONE', #25881 ) ;
#16655=ORIENTED_EDGE ( 'NONE', *, *, #36856, .T. ) ;
#16702=LINE ( 'NONE', #68207, #18905 ) ;
#16884=AXIS2_PLACEMENT_3D ( 'NONE', #41095, #56251, #28035 ) ;
#16928=AXIS2_PLACEMENT_3D ( 'NONE', #31745, #8083, #59980 ) ;
#16978=COLOUR_RGB ( '', 0.09019608, 0.27058824, 0.51372549) ;
#17007=EDGE_CURVE ( 'NONE', #65693, #57864, #1779, .T. ) ;
#17022=CARTESIAN_POINT ( 'NONE',  ( -8.637688417678548447, 13.69818742750669749, -55.00000000000000000 ) ) ;
#17047=CARTESIAN_POINT ( 'NONE',  ( 11.59999999999999787, 1.420590287010929336E-15, 53.20000000000001705 ) ) ;
#17086=CIRCLE ( 'NONE', #36284, 11.59999999999999787 ) ;
#17168=EDGE_CURVE ( 'NONE', #65977, #29431, #31059, .T. ) ;
#17186=FACE_OUTER_BOUND ( 'NONE', #25647, .T. ) ;
#17201=ORIENTED_EDGE ( 'NONE', *, *, #21047, .F. ) ;
#17261=CARTESIAN_POINT ( 'NONE',  ( -5.565113727472255967, 10.17789316117534248, -54.99999999999998579 ) ) ;
#17303=EDGE_LOOP ( 'NONE', ( #55852, #61883 ) ) ;
#17526=CIRCLE ( 'NONE', #35552, 11.59999999999999787 ) ;
#17649=AXIS2_PLACEMENT_3D ( 'NONE', #20439, #30591, #14423 ) ;
#17691=CARTESIAN_POINT ( 'NONE',  ( -8.637688417678550223, 13.69818742750669749, -44.99999999999998579 ) ) ;
#17722=ADVANCED_FACE ( 'NONE', ( #5403 ), #33568, .T. ) ;
#17762=CYLINDRICAL_SURFACE ( 'NONE', #31690, 12.49999999999999645 ) ;
#17861=CARTESIAN_POINT ( 'NONE',  ( 5.377855484467702900E-15, 4.693886760319831848E-15, 52.00000000000002132 ) ) ;
#17890=LINE ( 'NONE', #64880, #870 ) ;
#17891=CIRCLE ( 'NONE', #63585, 11.59999999999999787 ) ;
#17894=ADVANCED_FACE ( 'NONE', ( #521 ), #17762, .T. ) ;
#18072=CARTESIAN_POINT ( 'NONE',  ( 12.49999999999999645, 1.530808498934191127E-15, 125.0000000000000000 ) ) ;
#18075=DIRECTION ( 'NONE',  ( 1.000000000000000000, 0.000000000000000000, 0.000000000000000000 ) ) ;
#18263=CARTESIAN_POINT ( 'NONE',  ( 11.59999999999999787, 1.420590287010929336E-15, -54.99999999999998579 ) ) ;
#18287=DIRECTION ( 'NONE',  ( -1.000000000000000000, 0.000000000000000000, 0.000000000000000000 ) ) ;
#18302=LINE ( 'NONE', #52896, #69454 ) ;
#18306=DIRECTION ( 'NONE',  ( 1.000000000000000000, 0.000000000000000000, 0.000000000000000000 ) ) ;
#18394=DIRECTION ( 'NONE',  ( 0.000000000000000000, 0.000000000000000000, 1.000000000000000000 ) ) ;
#18495=PRODUCT_CONTEXT ( 'NONE', #40285, 'mechanical' ) ;
#18499=DIRECTION ( 'NONE',  ( 0.000000000000000000, 0.000000000000000000, 1.000000000000000000 ) ) ;
#18501=DIRECTION ( 'NONE',  ( 0.000000000000000000, 0.000000000000000000, 1.000000000000000000 ) ) ;
#18519=DIRECTION ( 'NONE',  ( -0.000000000000000000, -0.000000000000000000, -1.000000000000000000 ) ) ;
#18546=AXIS2_PLACEMENT_3D ( 'NONE', #70604, #65371, #52588 ) ;
#18624=DIRECTION ( 'NONE',  ( 0.7533909544171996098, 0.6575728627325955200, -7.625282249115660656E-32 ) ) ;
#18745=VECTOR ( 'NONE', #40636, 1000.000000000000000 ) ;
#18781=DIRECTION ( 'NONE',  ( -0.6575728627325957421, 0.7533909544171993877, 1.230411769795008318E-16 ) ) ;
#18802=DIRECTION ( 'NONE',  ( 0.000000000000000000, 0.000000000000000000, 1.000000000000000000 ) ) ;
#18825=CARTESIAN_POINT ( 'NONE',  ( -7.469491406282094736, 4.756046723998911929, 32.98187577049606745 ) ) ;
#18866=LINE ( 'NONE', #24886, #24754 ) ;
#18883=FACE_OUTER_BOUND ( 'NONE', #42101, .T. ) ;
#18905=VECTOR ( 'NONE', #39641, 1000.000000000000114 ) ;
#18923=ADVANCED_FACE ( 'NONE', ( #43782 ), #42660, .T. ) ;
#18980=DIRECTION ( 'NONE',  ( 0.000000000000000000, 0.000000000000000000, 1.000000000000000000 ) ) ;
#19069=DIRECTION ( 'NONE',  ( 0.000000000000000000, 0.000000000000000000, 1.000000000000000000 ) ) ;
#19136=DIRECTION ( 'NONE',  ( 1.000000000000000000, 0.000000000000000000, -0.000000000000000000 ) ) ;
#19234=CIRCLE ( 'NONE', #138, 12.49999999999999645 ) ;
#19330=DIRECTION ( 'NONE',  ( 0.000000000000000000, 0.000000000000000000, 1.000000000000000000 ) ) ;
#19463=EDGE_CURVE ( 'NONE', #61855, #58186, #25743, .T. ) ;
#19506=DIRECTION ( 'NONE',  ( -1.000000000000000000, 0.000000000000000000, 0.000000000000000000 ) ) ;
#19511=VERTEX_POINT ( 'NONE', #36406 ) ;
#19520=CARTESIAN_POINT ( 'NONE',  ( 0.000000000000000000, 0.000000000000000000, -44.99999999999998579 ) ) ;
#19551=CIRCLE ( 'NONE', #25567, 11.59999999999999787 ) ;
#19559=CARTESIAN_POINT ( 'NONE',  ( -11.59999999999999787, 0.000000000000000000, 53.20000000000001705 ) ) ;
#19564=CARTESIAN_POINT ( 'NONE',  ( -12.40464318976452596, 10.41032311384371489, 42.00000000000001421 ) ) ;
#19574=ADVANCED_FACE ( 'NONE', ( #64261 ), #41321, .F. ) ;
#19589=ADVANCED_FACE ( 'NONE', ( #46966 ), #12369, .F. ) ;
#19598=VECTOR ( 'NONE', #73266, 1000.000000000000000 ) ;
#19735=DIRECTION ( 'NONE',  ( 1.000000000000000000, 0.000000000000000000, 0.000000000000000000 ) ) ;
#19765=DIRECTION ( 'NONE',  ( 0.000000000000000000, 0.000000000000000000, 1.000000000000000000 ) ) ;
#19805=CARTESIAN_POINT ( 'NONE',  ( 0.000000000000000000, 0.000000000000000000, 40.80000000000001847 ) ) ;
#19906=DIRECTION ( 'NONE',  ( 0.000000000000000000, -1.000000000000000000, 0.000000000000000000 ) ) ;
#19917=CARTESIAN_POINT ( 'NONE',  ( -8.637688417678548447, 13.69818742750669749, -55.00000000000000000 ) ) ;
#20096=ORIENTED_EDGE ( 'NONE', *, *, #49978, .T. ) ;
#20108=CIRCLE ( 'NONE', #58533, 12.49999999999999645 ) ;
#20141=ORIENTED_EDGE ( 'NONE', *, *, #49978, .F. ) ;
#20147=CARTESIAN_POINT ( 'NONE',  ( -11.59999999999999787, 0.000000000000000000, -43.79999999999998295 ) ) ;
#20336=ORIENTED_EDGE ( 'NONE', *, *, #21047, .T. ) ;
#20439=CARTESIAN_POINT ( 'NONE',  ( -7.469491406282117829, 4.756046723998917258, -64.01812422950395387 ) ) ;
#20685=ORIENTED_EDGE ( 'NONE', *, *, #66868, .T. ) ;
#20835=ORIENTED_EDGE ( 'NONE', *, *, #15091, .T. ) ;
#20889=EDGE_LOOP ( 'NONE', ( #51992, #61101 ) ) ;
#21047=EDGE_CURVE ( 'NONE', #3438, #48900, #49402, .T. ) ;
#21090=VECTOR ( 'NONE', #7697, 1000.000000000000000 ) ;
#21145=ORIENTED_EDGE ( 'NONE', *, *, #46412, .F. ) ;
#21212=EDGE_CURVE ( 'NONE', #39181, #68344, #24814, .T. ) ;
#21271=DIRECTION ( 'NONE',  ( 1.000000000000000000, 0.000000000000000000, 0.000000000000000000 ) ) ;
#21460=CARTESIAN_POINT ( 'NONE',  ( 0.000000000000000000, 0.000000000000000000, 125.0000000000000000 ) ) ;
#21528=ORIENTED_EDGE ( 'NONE', *, *, #45538, .F. ) ;
#21612=ORIENTED_EDGE ( 'NONE', *, *, #19463, .T. ) ;
#21749=ADVANCED_FACE ( 'NONE', ( #54323 ), #72690, .T. ) ;
#21790=DIRECTION ( 'NONE',  ( 1.000000000000000000, 0.000000000000000000, 0.000000000000000000 ) ) ;
#21791=( GEOMETRIC_REPRESENTATION_CONTEXT ( 3 ) GLOBAL_UNCERTAINTY_ASSIGNED_CONTEXT ( ( #55031 ) ) GLOBAL_UNIT_ASSIGNED_CONTEXT ( ( #38147, #3228, #15590 ) ) REPRESENTATION_CONTEXT ( 'NONE', 'WORKASPACE' ) );
#21826=ORIENTED_EDGE ( 'NONE', *, *, #66540, .T. ) ;
#21853=FACE_OUTER_BOUND ( 'NONE', #61028, .T. ) ;
#21877=VERTEX_POINT ( 'NONE', #67822 ) ;
#21941=PLANE ( 'NONE',  #37962 ) ;
#22066=CIRCLE ( 'NONE', #5288, 11.59999999999999787 ) ;
#22097=AXIS2_PLACEMENT_3D ( 'NONE', #4658, #56140, #34315 ) ;
#22102=LINE ( 'NONE', #10071, #72976 ) ;
#22235=CYLINDRICAL_SURFACE ( 'NONE', #63965, 11.59999999999999787 ) ;
#22320=CARTESIAN_POINT ( 'NONE',  ( -11.59999999999999787, 0.000000000000000000, -43.79999999999998295 ) ) ;
#22395=EDGE_CURVE ( 'NONE', #2275, #26184, #12249, .T. ) ;
#22466=FACE_OUTER_BOUND ( 'NONE', #70693, .T. ) ;
#22490=CARTESIAN_POINT ( 'NONE',  ( -3.702536634196120335, 8.043911037661892749, -55.00000000000000000 ) ) ;
#22505=ORIENTED_EDGE ( 'NONE', *, *, #54343, .T. ) ;
#22547=DIRECTION ( 'NONE',  ( 0.000000000000000000, 0.000000000000000000, 1.000000000000000000 ) ) ;
#22607=DIRECTION ( 'NONE',  ( -0.000000000000000000, -0.000000000000000000, -1.000000000000000000 ) ) ;
#22706=AXIS2_PLACEMENT_3D ( 'NONE', #45519, #10534, #62818 ) ;
#22743=CARTESIAN_POINT ( 'NONE',  ( -3.702536634196095910, 8.043911037661889196, 52.00000000000002132 ) ) ;
#22777=ORIENTED_EDGE ( 'NONE', *, *, #15006, .T. ) ;
#22845=CYLINDRICAL_SURFACE ( 'NONE', #25563, 11.59999999999999787 ) ;
#22978=CARTESIAN_POINT ( 'NONE',  ( -5.565113727472241756, 10.17789316117534959, 42.00000000000001421 ) ) ;
#22988=FACE_OUTER_BOUND ( 'NONE', #38183, .T. ) ;
#23000=DIRECTION ( 'NONE',  ( -0.6575728627325955200, 0.7533909544171996098, 1.230411769795008318E-16 ) ) ;
#23307=ORIENTED_EDGE ( 'NONE', *, *, #10335, .F. ) ;
#23310=VECTOR ( 'NONE', #25972, 1000.000000000000000 ) ;
#23331=CARTESIAN_POINT ( 'NONE',  ( 0.000000000000000000, 0.000000000000000000, 125.0000000000000000 ) ) ;
#23399=ORIENTED_EDGE ( 'NONE', *, *, #47196, .T. ) ;
#23537=LINE ( 'NONE', #6618, #50835 ) ;
#23663=CARTESIAN_POINT ( 'NONE',  ( -7.469491406282116053, 4.756046723998915482, -45.00000000000000000 ) ) ;
#23732=FILL_AREA_STYLE_COLOUR ( '', #48977 ) ;
#23935=AXIS2_PLACEMENT_3D ( 'NONE', #12272, #40865, #18287 ) ;
#23936=ORIENTED_EDGE ( 'NONE', *, *, #30719, .F. ) ;
#24198=LINE ( 'NONE', #7273, #10632 ) ;
#24269=EDGE_LOOP ( 'NONE', ( #48986, #9258, #21612, #56889 ) ) ;
#24413=DIRECTION ( 'NONE',  ( 1.000000000000000000, 0.000000000000000000, 0.000000000000000000 ) ) ;
#24415=EDGE_LOOP ( 'NONE', ( #67017, #23307, #16179, #46125 ) ) ;
#24419=ORIENTED_EDGE ( 'NONE', *, *, #39161, .F. ) ;
#24428=ORIENTED_EDGE ( 'NONE', *, *, #74018, .T. ) ;
#24492=LINE ( 'NONE', #64356, #11830 ) ;
#24694=EDGE_CURVE ( 'NONE', #31534, #34228, #30863, .T. ) ;
#24708=CARTESIAN_POINT ( 'NONE',  ( -12.49999999999999645, 0.000000000000000000, 40.80000000000001847 ) ) ;
#24727=VERTEX_POINT ( 'NONE', #44017 ) ;
#24736=CARTESIAN_POINT ( 'NONE',  ( 0.000000000000000000, 0.000000000000000000, -54.99999999999998579 ) ) ;
#24738=CARTESIAN_POINT ( 'NONE',  ( 0.000000000000000000, 0.000000000000000000, -105.0000000000000000 ) ) ;
#24754=VECTOR ( 'NONE', #71103, 1000.000000000000000 ) ;
#24814=LINE ( 'NONE', #37219, #48262 ) ;
#24842=EDGE_CURVE ( 'NONE', #36680, #71004, #50003, .T. ) ;
#24845=LINE ( 'NONE', #7926, #37129 ) ;
#24886=CARTESIAN_POINT ( 'NONE',  ( -11.59999999999999787, 0.000000000000000000, 42.00000000000001421 ) ) ;
#24979=ADVANCED_FACE ( 'NONE', ( #39118, #10531 ), #33456, .T. ) ;
#24985=CARTESIAN_POINT ( 'NONE',  ( 6.782329983125267248, 10.49999999999999645, -105.0000000000000000 ) ) ;
#25031=ORIENTED_EDGE ( 'NONE', *, *, #48628, .T. ) ;
#25182=CARTESIAN_POINT ( 'NONE',  ( 11.59999999999999787, 1.420590287010929336E-15, -56.19999999999998863 ) ) ;
#25188=DIRECTION ( 'NONE',  ( 0.000000000000000000, 0.000000000000000000, 1.000000000000000000 ) ) ;
#25238=AXIS2_PLACEMENT_3D ( 'NONE', #56171, #51263, #50525 ) ;
#25255=ORIENTED_EDGE ( 'NONE', *, *, #24694, .T. ) ;
#25305=CARTESIAN_POINT ( 'NONE',  ( 0.000000000000000000, 0.000000000000000000, -105.0000000000000000 ) ) ;
#25344=ORIENTED_EDGE ( 'NONE', *, *, #47763, .T. ) ;
#25384=DIRECTION ( 'NONE',  ( 0.000000000000000000, 0.000000000000000000, 1.000000000000000000 ) ) ;
#25398=ADVANCED_FACE ( 'NONE', ( #5207 ), #26986, .T. ) ;
#25442=ORIENTED_EDGE ( 'NONE', *, *, #62559, .T. ) ;
#25551=LINE ( 'NONE', #65426, #28361 ) ;
#25557=EDGE_CURVE ( 'NONE', #45793, #1974, #65441, .T. ) ;
#25563=AXIS2_PLACEMENT_3D ( 'NONE', #28460, #29558, #52496 ) ;
#25567=AXIS2_PLACEMENT_3D ( 'NONE', #33599, #39258, #62186 ) ;
#25647=EDGE_LOOP ( 'NONE', ( #54095, #576 ) ) ;
#25652=EDGE_CURVE ( 'NONE', #31534, #14320, #35424, .T. ) ;
#25739=FACE_OUTER_BOUND ( 'NONE', #28548, .T. ) ;
#25743=CIRCLE ( 'NONE', #44965, 12.49999999999999645 ) ;
#25758=FILL_AREA_STYLE_COLOUR ( '', #16978 ) ;
#25862=VERTEX_POINT ( 'NONE', #9986 ) ;
#25865=CARTESIAN_POINT ( 'NONE',  ( 4.574237413256328308E-15, 3.992474787516289480E-15, 42.00000000000001421 ) ) ;
#25881=CARTESIAN_POINT ( 'NONE',  ( -12.49999999999999645, 0.000000000000000000, -43.79999999999998295 ) ) ;
#25950=LINE ( 'NONE', #19564, #31727 ) ;
#25972=DIRECTION ( 'NONE',  ( -0.6575728627325957421, 0.7533909544171994987, 0.000000000000000000 ) ) ;
#26033=CARTESIAN_POINT ( 'NONE',  ( -6.170112525937321735, 10.87104923258428180, -44.99999999999998579 ) ) ;
#26161=DIRECTION ( 'NONE',  ( 1.000000000000000000, 0.000000000000000000, 0.000000000000000000 ) ) ;
#26184=VERTEX_POINT ( 'NONE', #49385 ) ;
#26213=ORIENTED_EDGE ( 'NONE', *, *, #28341, .T. ) ;
#26469=ADVANCED_FACE ( 'NONE', ( #6857 ), #63652, .F. ) ;
#26522=DIRECTION ( 'NONE',  ( 1.000000000000000000, 0.000000000000000000, -0.000000000000000000 ) ) ;
#26530=VERTEX_POINT ( 'NONE', #37294 ) ;
#26535=EDGE_CURVE ( 'NONE', #65205, #21877, #18866, .T. ) ;
#26677=DIRECTION ( 'NONE',  ( 0.000000000000000000, 0.000000000000000000, -1.000000000000000000 ) ) ;
#26898=LINE ( 'NONE', #32538, #70606 ) ;
#26986=PLANE ( 'NONE',  #60614 ) ;
#27042=CARTESIAN_POINT ( 'NONE',  ( 0.000000000000000000, 0.000000000000000000, 53.20000000000001705 ) ) ;
#27122=CARTESIAN_POINT ( 'NONE',  ( 11.59999999999999787, 1.420590287010929336E-15, -54.99999999999998579 ) ) ;
#27241=VERTEX_POINT ( 'NONE', #10563 ) ;
#27444=EDGE_LOOP ( 'NONE', ( #42949, #61254, #60660, #31066 ) ) ;
#27578=FACE_OUTER_BOUND ( 'NONE', #66233, .T. ) ;
#27582=EDGE_CURVE ( 'NONE', #32702, #70313, #51272, .T. ) ;
#27696=CARTESIAN_POINT ( 'NONE',  ( -12.40464318976454727, 10.41032311384371667, -45.00000000000000000 ) ) ;
#27730=CARTESIAN_POINT ( 'NONE',  ( -11.59999999999999787, 0.000000000000000000, -54.99999999999998579 ) ) ;
#27779=DIRECTION ( 'NONE',  ( -0.6575728627325955200, 0.7533909544171997208, 0.000000000000000000 ) ) ;
#27901=CARTESIAN_POINT ( 'NONE',  ( 0.000000000000000000, 0.000000000000000000, 52.00000000000002132 ) ) ;
#28027=AXIS2_PLACEMENT_3D ( 'NONE', #3255, #19765, #26522 ) ;
#28035=DIRECTION ( 'NONE',  ( 1.000000000000000000, 0.000000000000000000, -0.000000000000000000 ) ) ;
#28081=DIRECTION ( 'NONE',  ( 0.000000000000000000, 0.000000000000000000, 1.000000000000000000 ) ) ;
#28128=AXIS2_PLACEMENT_3D ( 'NONE', #50754, #12381, #19136 ) ;
#28182=DIRECTION ( 'NONE',  ( 0.000000000000000000, 0.000000000000000000, 1.000000000000000000 ) ) ;
#28184=AXIS2_PLACEMENT_3D ( 'NONE', #51108, #22547, #68419 ) ;
#28202=CARTESIAN_POINT ( 'NONE',  ( -11.59999999999999787, 0.000000000000000000, 52.00000000000002132 ) ) ;
#28221=DIRECTION ( 'NONE',  ( 0.6575728627325955200, -0.7533909544171996098, 0.000000000000000000 ) ) ;
#28270=CARTESIAN_POINT ( 'NONE',  ( 6.782329983125267248, 10.49999999999999645, -105.0000000000000000 ) ) ;
#28327=CYLINDRICAL_SURFACE ( 'NONE', #25238, 12.49999999999999645 ) ;
#28341=EDGE_CURVE ( 'NONE', #58950, #21877, #71801, .T. ) ;
#28361=VECTOR ( 'NONE', #71403, 1000.000000000000000 ) ;
#28370=EDGE_LOOP ( 'NONE', ( #23936, #69220, #50376, #29299 ) ) ;
#28397=CIRCLE ( 'NONE', #70398, 11.59999999999999787 ) ;
#28431=CARTESIAN_POINT ( 'NONE',  ( -7.469491406282094736, 4.756046723998911929, 32.98187577049606745 ) ) ;
#28460=CARTESIAN_POINT ( 'NONE',  ( 0.000000000000000000, 0.000000000000000000, -43.79999999999998295 ) ) ;
#28548=EDGE_LOOP ( 'NONE', ( #51200, #8539 ) ) ;
#28912=EDGE_CURVE ( 'NONE', #25862, #34228, #68347, .T. ) ;
#28949=EDGE_LOOP ( 'NONE', ( #57525, #29495, #68705, #24419 ) ) ;
#28953=DIRECTION ( 'NONE',  ( 1.000000000000000000, 0.000000000000000000, 0.000000000000000000 ) ) ;
#28999=SURFACE_SIDE_STYLE ('',( #52675 ) ) ;
#29112=ORIENTED_EDGE ( 'NONE', *, *, #32603, .T. ) ;
#29154=LINE ( 'NONE', #1384, #579 ) ;
#29205=CIRCLE ( 'NONE', #42424, 12.49999999999999645 ) ;
#29224=CARTESIAN_POINT ( 'NONE',  ( -11.59999999999999787, 0.000000000000000000, 53.20000000000001705 ) ) ;
#29299=ORIENTED_EDGE ( 'NONE', *, *, #64767, .F. ) ;
#29369=EDGE_CURVE ( 'NONE', #71558, #1809, #30964, .T. ) ;
#29431=VERTEX_POINT ( 'NONE', #55160 ) ;
#29435=FACE_OUTER_BOUND ( 'NONE', #14416, .T. ) ;
#29437=DIRECTION ( 'NONE',  ( -0.000000000000000000, -0.000000000000000000, -1.000000000000000000 ) ) ;
#29495=ORIENTED_EDGE ( 'NONE', *, *, #41669, .T. ) ;
#29545=CIRCLE ( 'NONE', #45192, 11.59999999999999787 ) ;
#29558=DIRECTION ( 'NONE',  ( 0.000000000000000000, 0.000000000000000000, -1.000000000000000000 ) ) ;
#29582=ORIENTED_EDGE ( 'NONE', *, *, #2147, .T. ) ;
#29682=DIRECTION ( 'NONE',  ( 0.000000000000000000, 0.000000000000000000, 1.000000000000000000 ) ) ;
#29696=CARTESIAN_POINT ( 'NONE',  ( 0.000000000000000000, 0.000000000000000000, -44.99999999999998579 ) ) ;
#29758=VECTOR ( 'NONE', #40290, 1000.000000000000000 ) ;
#29770=DIRECTION ( 'NONE',  ( 1.000000000000000000, 0.000000000000000000, -0.000000000000000000 ) ) ;
#29805=ORIENTED_EDGE ( 'NONE', *, *, #718, .F. ) ;
#29893=ADVANCED_FACE ( 'NONE', ( #54702 ), #56838, .T. ) ;
#30007=ORIENTED_EDGE ( 'NONE', *, *, #10807, .T. ) ;
#30108=PLANE ( 'NONE',  #40329 ) ;
#30153=CARTESIAN_POINT ( 'NONE',  ( 0.000000000000000000, 0.000000000000000000, -125.0000000000000000 ) ) ;
#30183=EDGE_LOOP ( 'NONE', ( #47327, #24428, #25344, #40688 ) ) ;
#30223=EDGE_CURVE ( 'NONE', #26184, #35072, #13547, .T. ) ;
#30272=CARTESIAN_POINT ( 'NONE',  ( 0.000000000000000000, 0.000000000000000000, 40.80000000000001847 ) ) ;
#30277=CARTESIAN_POINT ( 'NONE',  ( 12.49999999999999645, 1.530808498934191127E-15, 40.80000000000001847 ) ) ;
#30323=DIRECTION ( 'NONE',  ( 0.000000000000000000, 0.000000000000000000, 1.000000000000000000 ) ) ;
#30338=DIRECTION ( 'NONE',  ( 0.000000000000000000, 0.000000000000000000, -1.000000000000000000 ) ) ;
#30378=EDGE_LOOP ( 'NONE', ( #13244, #14520, #45635, #59823 ) ) ;
#30471=( NAMED_UNIT ( * ) PLANE_ANGLE_UNIT ( ) SI_UNIT ( $, .RADIAN. ) );
#30472=DIRECTION ( 'NONE',  ( -0.6575728627325957421, 0.7533909544171994987, 0.000000000000000000 ) ) ;
#30591=DIRECTION ( 'NONE',  ( 0.6575728627325956310, -0.7533909544171997208, -1.230411769795008071E-16 ) ) ;
#30657=ADVANCED_FACE ( 'NONE', ( #46948 ), #52207, .T. ) ;
#30658=CIRCLE ( 'NONE', #70309, 11.59999999999999787 ) ;
#30675=CARTESIAN_POINT ( 'NONE',  ( -9.937067298023317008, 7.583184918921301865, -54.99999999999999289 ) ) ;
#30719=EDGE_CURVE ( 'NONE', #24727, #55701, #64601, .T. ) ;
#30725=AXIS2_PLACEMENT_3D ( 'NONE', #61660, #45875, #68041 ) ;
#30741=CARTESIAN_POINT ( 'NONE',  ( 6.782329983125267248, 10.49999999999999645, -125.0000000000000000 ) ) ;
#30749=AXIS2_PLACEMENT_3D ( 'NONE', #12491, #18499, #29770 ) ;
#30863=LINE ( 'NONE', #35413, #32883 ) ;
#30869=ORIENTED_EDGE ( 'NONE', *, *, #14946, .T. ) ;
#30904=ORIENTED_EDGE ( 'NONE', *, *, #50319, .F. ) ;
#30936=VECTOR ( 'NONE', #30338, 1000.000000000000000 ) ;
#30955=FACE_OUTER_BOUND ( 'NONE', #9488, .T. ) ;
#30962=CIRCLE ( 'NONE', #72979, 11.59999999999999787 ) ;
#30964=CIRCLE ( 'NONE', #68231, 12.49999999999999645 ) ;
#31020=AXIS2_PLACEMENT_3D ( 'NONE', #45957, #35032, #68881 ) ;
#31040=EDGE_LOOP ( 'NONE', ( #57841, #46453, #65928, #58421, #66875, #20141, #50015, #67618 ) ) ;
#31059=LINE ( 'NONE', #20147, #72249 ) ;
#31066=ORIENTED_EDGE ( 'NONE', *, *, #67721, .T. ) ;
#31106=CYLINDRICAL_SURFACE ( 'NONE', #61588, 11.59999999999999787 ) ;
#31115=DIRECTION ( 'NONE',  ( -1.000000000000000000, 0.000000000000000000, 0.000000000000000000 ) ) ;
#31133=DIRECTION ( 'NONE',  ( 0.000000000000000000, -0.000000000000000000, 1.000000000000000000 ) ) ;
#31145=ORIENTED_EDGE ( 'NONE', *, *, #58215, .F. ) ;
#31159=CYLINDRICAL_SURFACE ( 'NONE', #42934, 11.59999999999999787 ) ;
#31333=PRODUCT_DEFINITION_SHAPE ( 'NONE', 'NONE',  #6784 ) ;
#31356=EDGE_LOOP ( 'NONE', ( #60593, #47788 ) ) ;
#31371=CARTESIAN_POINT ( 'NONE',  ( 0.000000000000000000, 0.000000000000000000, -43.79999999999998295 ) ) ;
#31455=FACE_OUTER_BOUND ( 'NONE', #34266, .T. ) ;
#31512=CIRCLE ( 'NONE', #51968, 12.49999999999999645 ) ;
#31534=VERTEX_POINT ( 'NONE', #56852 ) ;
#31566=CIRCLE ( 'NONE', #59168, 12.49999999999999645 ) ;
#31690=AXIS2_PLACEMENT_3D ( 'NONE', #6138, #40707, #69996 ) ;
#31727=VECTOR ( 'NONE', #30472, 1000.000000000000000 ) ;
#31745=CARTESIAN_POINT ( 'NONE',  ( 0.000000000000000000, 0.000000000000000000, -54.99999999999998579 ) ) ;
#31747=ADVANCED_FACE ( 'NONE', ( #7192 ), #30108, .F. ) ;
#31756=LINE ( 'NONE', #60723, #73358 ) ;
#31800=ADVANCED_FACE ( 'NONE', ( #17186, #11172 ), #10423, .F. ) ;
#31982=ADVANCED_FACE ( 'NONE', ( #64525 ), #46132, .T. ) ;
#32058=ORIENTED_EDGE ( 'NONE', *, *, #62470, .F. ) ;
#32067=VECTOR ( 'NONE', #52414, 1000.000000000000000 ) ;
#32157=VERTEX_POINT ( 'NONE', #67488 ) ;
#32177=STYLED_ITEM ( 'NONE', ( #51934 ), #36653 ) ;
#32380=CARTESIAN_POINT ( 'NONE',  ( 0.000000000000000000, 0.000000000000000000, 42.00000000000001421 ) ) ;
#32440=ORIENTED_EDGE ( 'NONE', *, *, #3118, .F. ) ;
#32449=ORIENTED_EDGE ( 'NONE', *, *, #49056, .F. ) ;
#32538=CARTESIAN_POINT ( 'NONE',  ( -12.49999999999999645, 0.000000000000000000, 125.0000000000000000 ) ) ;
#32603=EDGE_CURVE ( 'NONE', #1809, #24727, #3160, .T. ) ;
#32702=VERTEX_POINT ( 'NONE', #50085 ) ;
#32765=EDGE_CURVE ( 'NONE', #26530, #58950, #24492, .T. ) ;
#32838=PRODUCT_DEFINITION_FORMATION_WITH_SPECIFIED_SOURCE ( 'ANY', '', #73401, .NOT_KNOWN. ) ;
#32883=VECTOR ( 'NONE', #52703, 1000.000000000000000 ) ;
#32952=CARTESIAN_POINT ( 'NONE',  ( 0.000000000000000000, 0.000000000000000000, -54.99999999999998579 ) ) ;
#33016=ORIENTED_EDGE ( 'NONE', *, *, #54175, .T. ) ;
#33119=CYLINDRICAL_SURFACE ( 'NONE', #66267, 11.59999999999999787 ) ;
#33144=DIRECTION ( 'NONE',  ( 1.000000000000000000, 0.000000000000000000, 0.000000000000000000 ) ) ;
#33266=CIRCLE ( 'NONE', #10482, 11.59999999999999787 ) ;
#33300=VERTEX_POINT ( 'NONE', #23663 ) ;
#33308=CARTESIAN_POINT ( 'NONE',  ( 12.49999999999999645, 1.530808498934191127E-15, 42.00000000000001421 ) ) ;
#33456=PLANE ( 'NONE',  #28128 ) ;
#33458=CIRCLE ( 'NONE', #39497, 12.49999999999999645 ) ;
#33568=CYLINDRICAL_SURFACE ( 'NONE', #22097, 12.49999999999999645 ) ;
#33599=CARTESIAN_POINT ( 'NONE',  ( 0.000000000000000000, 0.000000000000000000, 42.00000000000001421 ) ) ;
#33603=EDGE_LOOP ( 'NONE', ( #72856, #16655, #66265, #12310, #20336, #42553 ) ) ;
#33615=( LENGTH_UNIT ( ) NAMED_UNIT ( * ) SI_UNIT ( .MILLI., .METRE. ) );
#33704=DIRECTION ( 'NONE',  ( 0.6575728627325957421, -0.7533909544171993877, -1.230411769795008318E-16 ) ) ;
#33758=PLANE ( 'NONE',  #43470 ) ;
#33878=DIRECTION ( 'NONE',  ( -1.000000000000000000, 0.000000000000000000, 0.000000000000000000 ) ) ;
#33888=DIRECTION ( 'NONE',  ( 0.000000000000000000, 0.000000000000000000, 1.000000000000000000 ) ) ;
#34228=VERTEX_POINT ( 'NONE', #1983 ) ;
#34266=EDGE_LOOP ( 'NONE', ( #41255, #38110, #34496, #39715 ) ) ;
#34315=DIRECTION ( 'NONE',  ( -1.000000000000000000, 0.000000000000000000, 0.000000000000000000 ) ) ;
#34380=AXIS2_PLACEMENT_3D ( 'NONE', #25865, #31133, #60473 ) ;
#34478=CARTESIAN_POINT ( 'NONE',  ( -12.49999999999999645, 0.000000000000000000, 125.0000000000000000 ) ) ;
#34483=ORIENTED_EDGE ( 'NONE', *, *, #67553, .T. ) ;
#34496=ORIENTED_EDGE ( 'NONE', *, *, #66791, .T. ) ;
#34557=ORIENTED_EDGE ( 'NONE', *, *, #58215, .T. ) ;
#34569=EDGE_LOOP ( 'NONE', ( #52713, #30869 ) ) ;
#34597=CARTESIAN_POINT ( 'NONE',  ( -11.59999999999999787, 0.000000000000000000, 42.00000000000001421 ) ) ;
#34671=ORIENTED_EDGE ( 'NONE', *, *, #32603, .F. ) ;
#34676=ORIENTED_EDGE ( 'NONE', *, *, #4965, .F. ) ;
#34766=AXIS2_PLACEMENT_3D ( 'NONE', #43548, #60098, #54437 ) ;
#34967=ORIENTED_EDGE ( 'NONE', *, *, #27582, .F. ) ;
#34968=ADVANCED_FACE ( 'NONE', ( #4514 ), #50719, .F. ) ;
#35007=MECHANICAL_DESIGN_GEOMETRIC_PRESENTATION_REPRESENTATION('',(#54171),#57822);
#35011=PLANE ( 'NONE',  #65791 ) ;
#35032=DIRECTION ( 'NONE',  ( 0.000000000000000000, 0.000000000000000000, 1.000000000000000000 ) ) ;
#35072=VERTEX_POINT ( 'NONE', #17261 ) ;
#35120=VECTOR ( 'NONE', #71671, 1000.000000000000000 ) ;
#35139=ORIENTED_EDGE ( 'NONE', *, *, #68502, .T. ) ;
#35188=DIRECTION ( 'NONE',  ( 0.000000000000000000, 0.000000000000000000, 1.000000000000000000 ) ) ;
#35413=CARTESIAN_POINT ( 'NONE',  ( 12.49999999999999645, 1.530808498934191127E-15, 125.0000000000000000 ) ) ;
#35424=CIRCLE ( 'NONE', #72596, 12.49999999999999645 ) ;
#35551=DIRECTION ( 'NONE',  ( 1.000000000000000000, 0.000000000000000000, 0.000000000000000000 ) ) ;
#35552=AXIS2_PLACEMENT_3D ( 'NONE', #30272, #47572, #2501 ) ;
#35707=EDGE_LOOP ( 'NONE', ( #38818, #45027, #9210, #22505 ) ) ;
#35913=DIRECTION ( 'NONE',  ( 1.000000000000000000, 0.000000000000000000, 0.000000000000000000 ) ) ;
#36096=LINE ( 'NONE', #18072, #18745 ) ;
#36110=CARTESIAN_POINT ( 'NONE',  ( 0.000000000000000000, 0.000000000000000000, -56.19999999999998863 ) ) ;
#36141=AXIS2_PLACEMENT_3D ( 'NONE', #58188, #12322, #58553 ) ;
#36284=AXIS2_PLACEMENT_3D ( 'NONE', #31371, #54684, #59591 ) ;
#36288=DIRECTION ( 'NONE',  ( -0.000000000000000000, -0.000000000000000000, -1.000000000000000000 ) ) ;
#36305=VECTOR ( 'NONE', #4079, 1000.000000000000000 ) ;
#36406=CARTESIAN_POINT ( 'NONE',  ( -12.49999999999999645, 0.000000000000000000, 125.0000000000000000 ) ) ;
#36488=EDGE_CURVE ( 'NONE', #3181, #42920, #67372, .T. ) ;
#36574=AXIS2_PLACEMENT_3D ( 'NONE', #771, #46590, #2244 ) ;
#36653=MANIFOLD_SOLID_BREP ( 'Cut-Extrude1', #37993 ) ;
#36680=VERTEX_POINT ( 'NONE', #12812 ) ;
#36776=EDGE_LOOP ( 'NONE', ( #21528, #10263, #52116, #8807, #37651, #49073, #57377, #65408 ) ) ;
#36856=EDGE_CURVE ( 'NONE', #12834, #33300, #57132, .T. ) ;
#36942=CARTESIAN_POINT ( 'NONE',  ( -7.469491406282094736, 4.756046723998911929, 52.00000000000002132 ) ) ;
#36977=DIRECTION ( 'NONE',  ( 0.6575728627325956310, -0.7533909544171996098, 0.000000000000000000 ) ) ;
#37129=VECTOR ( 'NONE', #14306, 1000.000000000000000 ) ;
#37133=DIRECTION ( 'NONE',  ( 0.000000000000000000, 0.000000000000000000, 1.000000000000000000 ) ) ;
#37144=CARTESIAN_POINT ( 'NONE',  ( -5.565113727472242644, 10.17789316117535137, 52.00000000000002132 ) ) ;
#37154=CYLINDRICAL_SURFACE ( 'NONE', #34766, 11.59999999999999787 ) ;
#37163=EDGE_CURVE ( 'NONE', #35072, #3438, #61121, .T. ) ;
#37219=CARTESIAN_POINT ( 'NONE',  ( -11.59999999999999787, 0.000000000000000000, -54.99999999999998579 ) ) ;
#37294=CARTESIAN_POINT ( 'NONE',  ( 11.59999999999999787, 1.420590287010929336E-15, 42.00000000000001421 ) ) ;
#37316=VERTEX_POINT ( 'NONE', #22743 ) ;
#37341=ORIENTED_EDGE ( 'NONE', *, *, #62470, .T. ) ;
#37352=ORIENTED_EDGE ( 'NONE', *, *, #2882, .T. ) ;
#37403=DIRECTION ( 'NONE',  ( -0.000000000000000000, -0.000000000000000000, -1.000000000000000000 ) ) ;
#37568=ORIENTED_EDGE ( 'NONE', *, *, #11301, .T. ) ;
#37651=ORIENTED_EDGE ( 'NONE', *, *, #66868, .F. ) ;
#37772=EDGE_CURVE ( 'NONE', #26530, #63730, #29545, .T. ) ;
#37962=AXIS2_PLACEMENT_3D ( 'NONE', #38494, #5043, #9913 ) ;
#37993=CLOSED_SHELL ( 'NONE', ( #66476, #56216, #17894, #66074, #15532, #4301, #48387, #21749, #44820, #11605, #18923, #26469, #25398, #38375, #40994, #55186, #13644, #38028, #31747, #29893, #31800, #55649, #15808, #17722, #19574, #54596, #54246, #68021, #72532, #5055, #2193, #53997, #30657, #43219, #60434, #19589, #6615, #24979, #31982, #73129, #55791, #34968 ) ) ;
#38028=ADVANCED_FACE ( 'NONE', ( #38732 ), #73663, .F. ) ;
#38038=ORIENTED_EDGE ( 'NONE', *, *, #12890, .T. ) ;
#38110=ORIENTED_EDGE ( 'NONE', *, *, #43882, .F. ) ;
#38147=( LENGTH_UNIT ( ) NAMED_UNIT ( * ) SI_UNIT ( .MILLI., .METRE. ) );
#38183=EDGE_LOOP ( 'NONE', ( #9061, #44940, #45235, #65413 ) ) ;
#38294=ORIENTED_EDGE ( 'NONE', *, *, #29369, .T. ) ;
#38375=ADVANCED_FACE ( 'NONE', ( #59723 ), #3711, .T. ) ;
#38494=CARTESIAN_POINT ( 'NONE',  ( -1.734723475976807094E-14, 1.040834085586084257E-14, -45.00000000000000000 ) ) ;
#38605=AXIS2_PLACEMENT_3D ( 'NONE', #21460, #72227, #39145 ) ;
#38618=EDGE_CURVE ( 'NONE', #3181, #40171, #60901, .T. ) ;
#38732=FACE_OUTER_BOUND ( 'NONE', #59095, .T. ) ;
#38756=CARTESIAN_POINT ( 'NONE',  ( -12.49999999999999645, 0.000000000000000000, -56.19999999999998863 ) ) ;
#38803=DIRECTION ( 'NONE',  ( 1.000000000000000000, 0.000000000000000000, 0.000000000000000000 ) ) ;
#38818=ORIENTED_EDGE ( 'NONE', *, *, #54865, .F. ) ;
#38986=DIRECTION ( 'NONE',  ( 0.000000000000000000, 0.000000000000000000, 1.000000000000000000 ) ) ;
#39017=LINE ( 'NONE', #34478, #2123 ) ;
#39101=AXIS2_PLACEMENT_3D ( 'NONE', #3575, #65603, #48673 ) ;
#39118=FACE_OUTER_BOUND ( 'NONE', #31356, .T. ) ;
#39145=DIRECTION ( 'NONE',  ( -1.000000000000000000, 0.000000000000000000, 0.000000000000000000 ) ) ;
#39161=EDGE_CURVE ( 'NONE', #72303, #16639, #39017, .T. ) ;
#39181=VERTEX_POINT ( 'NONE', #27730 ) ;
#39208=ORIENTED_EDGE ( 'NONE', *, *, #30223, .F. ) ;
#39258=DIRECTION ( 'NONE',  ( 0.000000000000000000, 0.000000000000000000, 1.000000000000000000 ) ) ;
#39272=( NAMED_UNIT ( * ) SI_UNIT ( $, .STERADIAN. ) SOLID_ANGLE_UNIT ( ) );
#39497=AXIS2_PLACEMENT_3D ( 'NONE', #73370, #15875, #38803 ) ;
#39530=DIRECTION ( 'NONE',  ( 0.000000000000000000, 0.000000000000000000, 1.000000000000000000 ) ) ;
#39549=CIRCLE ( 'NONE', #7127, 11.59999999999999787 ) ;
#39568=ORIENTED_EDGE ( 'NONE', *, *, #52786, .F. ) ;
#39641=DIRECTION ( 'NONE',  ( -0.6575728627325955200, 0.7533909544171996098, 1.230411769795008318E-16 ) ) ;
#39676=ORIENTED_EDGE ( 'NONE', *, *, #61197, .T. ) ;
#39715=ORIENTED_EDGE ( 'NONE', *, *, #46412, .T. ) ;
#39717=VERTEX_POINT ( 'NONE', #52329 ) ;
#39784=FACE_OUTER_BOUND ( 'NONE', #34569, .T. ) ;
#39842=CARTESIAN_POINT ( 'NONE',  ( 0.000000000000000000, 0.000000000000000000, -44.99999999999998579 ) ) ;
#39915=AXIS2_PLACEMENT_3D ( 'NONE', #41629, #42380, #64949 ) ;
#39921=CARTESIAN_POINT ( 'NONE',  ( -8.637688417678550223, 13.69818742750669749, -64.01812422950393966 ) ) ;
#40131=EDGE_CURVE ( 'NONE', #40171, #41715, #72997, .T. ) ;
#40171=VERTEX_POINT ( 'NONE', #28202 ) ;
#40262=CYLINDRICAL_SURFACE ( 'NONE', #51173, 12.49999999999999645 ) ;
#40278=FACE_OUTER_BOUND ( 'NONE', #54447, .T. ) ;
#40285=APPLICATION_CONTEXT ( 'automotive_design' ) ;
#40290=DIRECTION ( 'NONE',  ( 0.6575728627325957421, -0.7533909544171994987, 0.000000000000000000 ) ) ;
#40329=AXIS2_PLACEMENT_3D ( 'NONE', #18825, #64710, #13193 ) ;
#40466=ORIENTED_EDGE ( 'NONE', *, *, #36856, .F. ) ;
#40636=DIRECTION ( 'NONE',  ( -0.000000000000000000, -0.000000000000000000, -1.000000000000000000 ) ) ;
#40637=CARTESIAN_POINT ( 'NONE',  ( 0.000000000000000000, 0.000000000000000000, -44.99999999999998579 ) ) ;
#40646=CIRCLE ( 'NONE', #31020, 12.49999999999999645 ) ;
#40688=ORIENTED_EDGE ( 'NONE', *, *, #67758, .F. ) ;
#40699=VECTOR ( 'NONE', #41749, 1000.000000000000114 ) ;
#40707=DIRECTION ( 'NONE',  ( -0.000000000000000000, -0.000000000000000000, -1.000000000000000000 ) ) ;
#40865=DIRECTION ( 'NONE',  ( 0.000000000000000000, 0.000000000000000000, -1.000000000000000000 ) ) ;
#40945=AXIS2_PLACEMENT_3D ( 'NONE', #25305, #66273, #48952 ) ;
#40994=ADVANCED_FACE ( 'NONE', ( #31455 ), #48749, .T. ) ;
#41095=CARTESIAN_POINT ( 'NONE',  ( 0.000000000000000000, 0.000000000000000000, -44.99999999999998579 ) ) ;
#41104=CARTESIAN_POINT ( 'NONE',  ( 11.59999999999999787, 1.420590287010929336E-15, 52.00000000000002132 ) ) ;
#41229=DIRECTION ( 'NONE',  ( 1.000000000000000000, 0.000000000000000000, 0.000000000000000000 ) ) ;
#41255=ORIENTED_EDGE ( 'NONE', *, *, #62860, .F. ) ;
#41277=CARTESIAN_POINT ( 'NONE',  ( 0.000000000000000000, 0.000000000000000000, -56.19999999999998863 ) ) ;
#41321=PLANE ( 'NONE',  #36574 ) ;
#41379=CARTESIAN_POINT ( 'NONE',  ( -6.782329983125267248, 10.49999999999999645, -125.0000000000000000 ) ) ;
#41629=CARTESIAN_POINT ( 'NONE',  ( 0.000000000000000000, 0.000000000000000000, 40.80000000000001847 ) ) ;
#41669=EDGE_CURVE ( 'NONE', #50389, #986, #58378, .T. ) ;
#41715=VERTEX_POINT ( 'NONE', #41104 ) ;
#41749=DIRECTION ( 'NONE',  ( 0.6575728627325955200, -0.7533909544171996098, -1.230411769795008318E-16 ) ) ;
#41941=AXIS2_PLACEMENT_3D ( 'NONE', #58668, #18802, #53035 ) ;
#42098=AXIS2_PLACEMENT_3D ( 'NONE', #7363, #35188, #35551 ) ;
#42101=EDGE_LOOP ( 'NONE', ( #51440, #32449, #38038, #8613 ) ) ;
#42157=DIRECTION ( 'NONE',  ( 0.000000000000000000, 0.000000000000000000, 1.000000000000000000 ) ) ;
#42210=CARTESIAN_POINT ( 'NONE',  ( -9.937067298023317008, 7.583184918921300977, -44.99999999999998579 ) ) ;
#42380=DIRECTION ( 'NONE',  ( 0.000000000000000000, 0.000000000000000000, 1.000000000000000000 ) ) ;
#42424=AXIS2_PLACEMENT_3D ( 'NONE', #36110, #46653, #47031 ) ;
#42439=EDGE_CURVE ( 'NONE', #41715, #1281, #16248, .T. ) ;
#42553=ORIENTED_EDGE ( 'NONE', *, *, #53884, .F. ) ;
#42660=CYLINDRICAL_SURFACE ( 'NONE', #10290, 12.49999999999999645 ) ;
#42734=CARTESIAN_POINT ( 'NONE',  ( 12.49999999999999645, 1.530808498934191127E-15, 125.0000000000000000 ) ) ;
#42737=VERTEX_POINT ( 'NONE', #62582 ) ;
#42920=VERTEX_POINT ( 'NONE', #36942 ) ;
#42934=AXIS2_PLACEMENT_3D ( 'NONE', #58623, #7861, #19506 ) ;
#42949=ORIENTED_EDGE ( 'NONE', *, *, #32765, .F. ) ;
#43098=AXIS2_PLACEMENT_3D ( 'NONE', #50168, #73102, #9600 ) ;
#43104=VERTEX_POINT ( 'NONE', #27122 ) ;
#43133=CARTESIAN_POINT ( 'NONE',  ( 0.000000000000000000, 0.000000000000000000, 125.0000000000000000 ) ) ;
#43180=VECTOR ( 'NONE', #31115, 1000.000000000000000 ) ;
#43219=ADVANCED_FACE ( 'NONE', ( #40278 ), #35011, .F. ) ;
#43268=CARTESIAN_POINT ( 'NONE',  ( 0.000000000000000000, 0.000000000000000000, -43.79999999999998295 ) ) ;
#43395=AXIS2_PLACEMENT_3D ( 'NONE', #48320, #71232, #19735 ) ;
#43470=AXIS2_PLACEMENT_3D ( 'NONE', #57812, #6318, #56331 ) ;
#43548=CARTESIAN_POINT ( 'NONE',  ( 0.000000000000000000, 0.000000000000000000, 53.20000000000001705 ) ) ;
#43579=ORIENTED_EDGE ( 'NONE', *, *, #49703, .F. ) ;
#43667=AXIS2_PLACEMENT_3D ( 'NONE', #6630, #63790, #47225 ) ;
#43735=DIRECTION ( 'NONE',  ( 0.000000000000000000, 0.000000000000000000, 1.000000000000000000 ) ) ;
#43782=FACE_OUTER_BOUND ( 'NONE', #10547, .T. ) ;
#43849=AXIS2_PLACEMENT_3D ( 'NONE', #71598, #12975, #54330 ) ;
#43882=EDGE_CURVE ( 'NONE', #5740, #65693, #33458, .T. ) ;
#44017=CARTESIAN_POINT ( 'NONE',  ( 6.782329983125267248, 10.49999999999999645, -125.0000000000000000 ) ) ;
#44072=CARTESIAN_POINT ( 'NONE',  ( 0.000000000000000000, 0.000000000000000000, -54.99999999999998579 ) ) ;
#44370=AXIS2_PLACEMENT_3D ( 'NONE', #10417, #28081, #73944 ) ;
#44433=EDGE_CURVE ( 'NONE', #29431, #66920, #39549, .T. ) ;
#44543=( NAMED_UNIT ( * ) PLANE_ANGLE_UNIT ( ) SI_UNIT ( $, .RADIAN. ) );
#44587=CIRCLE ( 'NONE', #36141, 12.49999999999999645 ) ;
#44670=DIRECTION ( 'NONE',  ( -0.000000000000000000, -0.000000000000000000, -1.000000000000000000 ) ) ;
#44717=CARTESIAN_POINT ( 'NONE',  ( -8.637688417678527131, 13.69818742750669394, 52.00000000000002132 ) ) ;
#44820=ADVANCED_FACE ( 'NONE', ( #60462 ), #37154, .T. ) ;
#44841=CIRCLE ( 'NONE', #43667, 12.49999999999999645 ) ;
#44849=EDGE_CURVE ( 'NONE', #34228, #24727, #67229, .T. ) ;
#44940=ORIENTED_EDGE ( 'NONE', *, *, #71022, .F. ) ;
#44965=AXIS2_PLACEMENT_3D ( 'NONE', #4535, #28182, #74043 ) ;
#44977=PLANE ( 'NONE',  #16884 ) ;
#45025=DIRECTION ( 'NONE',  ( 1.000000000000000000, 0.000000000000000000, -0.000000000000000000 ) ) ;
#45027=ORIENTED_EDGE ( 'NONE', *, *, #62151, .F. ) ;
#45112=CARTESIAN_POINT ( 'NONE',  ( -12.40464318976454727, 10.41032311384371667, -45.00000000000000000 ) ) ;
#45192=AXIS2_PLACEMENT_3D ( 'NONE', #53426, #42157, #58327 ) ;
#45235=ORIENTED_EDGE ( 'NONE', *, *, #3118, .T. ) ;
#45262=CARTESIAN_POINT ( 'NONE',  ( -7.469491406282094736, 4.756046723998911929, 52.00000000000002132 ) ) ;
#45277=FACE_OUTER_BOUND ( 'NONE', #47710, .T. ) ;
#45369=EDGE_LOOP ( 'NONE', ( #11482, #59375, #9255, #53101 ) ) ;
#45454=CARTESIAN_POINT ( 'NONE',  ( -6.170112525937310188, 10.87104923258429068, 125.0000000000000000 ) ) ;
#45519=CARTESIAN_POINT ( 'NONE',  ( 0.000000000000000000, 0.000000000000000000, 52.00000000000002132 ) ) ;
#45538=EDGE_CURVE ( 'NONE', #5740, #3181, #24845, .T. ) ;
#45604=EDGE_LOOP ( 'NONE', ( #53543, #70820, #2425, #30007 ) ) ;
#45612=LINE ( 'NONE', #17022, #46519 ) ;
#45635=ORIENTED_EDGE ( 'NONE', *, *, #67376, .F. ) ;
#45652=DIRECTION ( 'NONE',  ( 0.000000000000000000, 0.000000000000000000, 1.000000000000000000 ) ) ;
#45692=ORIENTED_EDGE ( 'NONE', *, *, #69033, .T. ) ;
#45740=EDGE_LOOP ( 'NONE', ( #57702, #872, #29582, #43579 ) ) ;
#45749=DIRECTION ( 'NONE',  ( 0.000000000000000000, 0.000000000000000000, 1.000000000000000000 ) ) ;
#45782=VERTEX_POINT ( 'NONE', #4531 ) ;
#45793=VERTEX_POINT ( 'NONE', #7808 ) ;
#45822=ORIENTED_EDGE ( 'NONE', *, *, #45538, .T. ) ;
#45841=LINE ( 'NONE', #5615, #19598 ) ;
#45875=DIRECTION ( 'NONE',  ( 0.7533909544171998318, 0.6575728627325954090, 0.000000000000000000 ) ) ;
#45957=CARTESIAN_POINT ( 'NONE',  ( 0.000000000000000000, 0.000000000000000000, -43.79999999999998295 ) ) ;
#46019=DIRECTION ( 'NONE',  ( -1.000000000000000000, 0.000000000000000000, 0.000000000000000000 ) ) ;
#46125=ORIENTED_EDGE ( 'NONE', *, *, #54175, .F. ) ;
#46132=CYLINDRICAL_SURFACE ( 'NONE', #23935, 11.59999999999999787 ) ;
#46154=CARTESIAN_POINT ( 'NONE',  ( 0.000000000000000000, 0.000000000000000000, 53.20000000000001705 ) ) ;
#46184=AXIS2_PLACEMENT_3D ( 'NONE', #52511, #30323, #18306 ) ;
#46272=DIRECTION ( 'NONE',  ( 1.000000000000000000, 0.000000000000000000, 0.000000000000000000 ) ) ;
#46279=CARTESIAN_POINT ( 'NONE',  ( 0.000000000000000000, 0.000000000000000000, 53.20000000000001705 ) ) ;
#46412=EDGE_CURVE ( 'NONE', #71004, #47656, #50423, .T. ) ;
#46453=ORIENTED_EDGE ( 'NONE', *, *, #52786, .T. ) ;
#46519=VECTOR ( 'NONE', #50851, 1000.000000000000114 ) ;
#46590=DIRECTION ( 'NONE',  ( 0.000000000000000000, 0.000000000000000000, 1.000000000000000000 ) ) ;
#46602=CARTESIAN_POINT ( 'NONE',  ( 0.000000000000000000, 0.000000000000000000, 125.0000000000000000 ) ) ;
#46653=DIRECTION ( 'NONE',  ( 0.000000000000000000, 0.000000000000000000, 1.000000000000000000 ) ) ;
#46919=CARTESIAN_POINT ( 'NONE',  ( -12.49999999999999645, 0.000000000000000000, 52.00000000000002132 ) ) ;
#46948=FACE_OUTER_BOUND ( 'NONE', #12302, .T. ) ;
#46953=CARTESIAN_POINT ( 'NONE',  ( -12.49999999999999645, 0.000000000000000000, -54.99999999999998579 ) ) ;
#46966=FACE_OUTER_BOUND ( 'NONE', #33603, .T. ) ;
#47008=AXIS2_PLACEMENT_3D ( 'NONE', #27042, #61282, #67286 ) ;
#47031=DIRECTION ( 'NONE',  ( 1.000000000000000000, 0.000000000000000000, 0.000000000000000000 ) ) ;
#47086=ORIENTED_EDGE ( 'NONE', *, *, #24842, .T. ) ;
#47088=SHAPE_DEFINITION_REPRESENTATION ( #31333, #8524 ) ;
#47118=EDGE_CURVE ( 'NONE', #68424, #19511, #19234, .T. ) ;
#47196=EDGE_CURVE ( 'NONE', #62456, #12834, #6073, .T. ) ;
#47225=DIRECTION ( 'NONE',  ( 1.000000000000000000, 0.000000000000000000, 0.000000000000000000 ) ) ;
#47297=EDGE_LOOP ( 'NONE', ( #955, #63177 ) ) ;
#47327=ORIENTED_EDGE ( 'NONE', *, *, #67376, .T. ) ;
#47372=ORIENTED_EDGE ( 'NONE', *, *, #12890, .F. ) ;
#47384=DIRECTION ( 'NONE',  ( 0.000000000000000000, 0.000000000000000000, -1.000000000000000000 ) ) ;
#47472=DIRECTION ( 'NONE',  ( -0.000000000000000000, -0.000000000000000000, -1.000000000000000000 ) ) ;
#47572=DIRECTION ( 'NONE',  ( 0.000000000000000000, 0.000000000000000000, 1.000000000000000000 ) ) ;
#47656=VERTEX_POINT ( 'NONE', #54315 ) ;
#47666=DIRECTION ( 'NONE',  ( -0.000000000000000000, 0.000000000000000000, -1.000000000000000000 ) ) ;
#47684=DIRECTION ( 'NONE',  ( 0.000000000000000000, 0.000000000000000000, 1.000000000000000000 ) ) ;
#47710=EDGE_LOOP ( 'NONE', ( #56606, #29805, #25442, #49777 ) ) ;
#47763=EDGE_CURVE ( 'NONE', #42920, #37316, #3937, .T. ) ;
#47788=ORIENTED_EDGE ( 'NONE', *, *, #25652, .T. ) ;
#47939=AXIS2_PLACEMENT_3D ( 'NONE', #8417, #14782, #36977 ) ;
#48039=DIRECTION ( 'NONE',  ( -1.000000000000000000, 0.000000000000000000, 0.000000000000000000 ) ) ;
#48148=VERTEX_POINT ( 'NONE', #42210 ) ;
#48262=VECTOR ( 'NONE', #47384, 1000.000000000000000 ) ;
#48301=ORIENTED_EDGE ( 'NONE', *, *, #51638, .T. ) ;
#48320=CARTESIAN_POINT ( 'NONE',  ( 0.000000000000000000, 0.000000000000000000, 0.000000000000000000 ) ) ;
#48387=ADVANCED_FACE ( 'NONE', ( #9456 ), #33119, .T. ) ;
#48495=FACE_OUTER_BOUND ( 'NONE', #58996, .T. ) ;
#48628=EDGE_CURVE ( 'NONE', #63730, #7618, #62331, .T. ) ;
#48673=DIRECTION ( 'NONE',  ( 1.000000000000000000, 0.000000000000000000, -0.000000000000000000 ) ) ;
#48715=PLANE ( 'NONE',  #28027 ) ;
#48749=CYLINDRICAL_SURFACE ( 'NONE', #10774, 12.49999999999999645 ) ;
#48761=ORIENTED_EDGE ( 'NONE', *, *, #12246, .F. ) ;
#48900=VERTEX_POINT ( 'NONE', #30675 ) ;
#48952=DIRECTION ( 'NONE',  ( 1.000000000000000000, 0.000000000000000000, -0.000000000000000000 ) ) ;
#48977=COLOUR_RGB ( '', 0.09019608, 0.27058824, 0.51372549) ;
#48986=ORIENTED_EDGE ( 'NONE', *, *, #15284, .F. ) ;
#49031=VECTOR ( 'NONE', #55744, 1000.000000000000000 ) ;
#49056=EDGE_CURVE ( 'NONE', #39717, #32702, #31512, .T. ) ;
#49073=ORIENTED_EDGE ( 'NONE', *, *, #42439, .F. ) ;
#49104=ORIENTED_EDGE ( 'NONE', *, *, #14410, .F. ) ;
#49177=ORIENTED_EDGE ( 'NONE', *, *, #39161, .T. ) ;
#49197=EDGE_CURVE ( 'NONE', #63730, #36680, #19551, .T. ) ;
#49385=CARTESIAN_POINT ( 'NONE',  ( -6.170112525937322623, 10.87104923258428180, -54.99999999999998579 ) ) ;
#49402=LINE ( 'NONE', #73054, #61479 ) ;
#49497=DIRECTION ( 'NONE',  ( 1.000000000000000000, 0.000000000000000000, 0.000000000000000000 ) ) ;
#49703=EDGE_CURVE ( 'NONE', #19511, #45782, #45841, .T. ) ;
#49777=ORIENTED_EDGE ( 'NONE', *, *, #28912, .T. ) ;
#49921=DIRECTION ( 'NONE',  ( 0.7533909544171996098, 0.6575728627325955200, -7.625282249115660656E-32 ) ) ;
#49978=EDGE_CURVE ( 'NONE', #66920, #62456, #68886, .T. ) ;
#50003=LINE ( 'NONE', #54550, #23310 ) ;
#50015=ORIENTED_EDGE ( 'NONE', *, *, #44433, .F. ) ;
#50018=ORIENTED_EDGE ( 'NONE', *, *, #67758, .T. ) ;
#50061=EDGE_CURVE ( 'NONE', #48148, #12834, #67551, .T. ) ;
#50085=CARTESIAN_POINT ( 'NONE',  ( 12.49999999999999645, 1.530808498934191127E-15, -44.99999999999998579 ) ) ;
#50168=CARTESIAN_POINT ( 'NONE',  ( 0.000000000000000000, 0.000000000000000000, -54.99999999999998579 ) ) ;
#50287=DIRECTION ( 'NONE',  ( 0.000000000000000000, 0.000000000000000000, -1.000000000000000000 ) ) ;
#50319=EDGE_CURVE ( 'NONE', #33300, #42737, #23537, .T. ) ;
#50376=ORIENTED_EDGE ( 'NONE', *, *, #28912, .F. ) ;
#50389=VERTEX_POINT ( 'NONE', #30277 ) ;
#50423=CIRCLE ( 'NONE', #70807, 12.49999999999999645 ) ;
#50467=VECTOR ( 'NONE', #52091, 1000.000000000000000 ) ;
#50515=ORIENTED_EDGE ( 'NONE', *, *, #41669, .F. ) ;
#50525=DIRECTION ( 'NONE',  ( -1.000000000000000000, 0.000000000000000000, 0.000000000000000000 ) ) ;
#50553=VERTEX_POINT ( 'NONE', #59990 ) ;
#50719=PLANE ( 'NONE',  #40945 ) ;
#50754=CARTESIAN_POINT ( 'NONE',  ( 0.000000000000000000, 0.000000000000000000, -56.19999999999998863 ) ) ;
#50808=APPLICATION_CONTEXT ( 'automotive_design' ) ;
#50835=VECTOR ( 'NONE', #18624, 1000.000000000000114 ) ;
#50851=DIRECTION ( 'NONE',  ( 0.6575728627325955200, -0.7533909544171996098, -1.230411769795008318E-16 ) ) ;
#51108=CARTESIAN_POINT ( 'NONE',  ( 0.000000000000000000, 0.000000000000000000, -56.19999999999998863 ) ) ;
#51173=AXIS2_PLACEMENT_3D ( 'NONE', #63211, #22607, #33878 ) ;
#51200=ORIENTED_EDGE ( 'NONE', *, *, #51638, .F. ) ;
#51263=DIRECTION ( 'NONE',  ( -0.000000000000000000, -0.000000000000000000, -1.000000000000000000 ) ) ;
#51271=DIRECTION ( 'NONE',  ( 0.000000000000000000, 0.000000000000000000, 1.000000000000000000 ) ) ;
#51272=CIRCLE ( 'NONE', #66887, 12.49999999999999645 ) ;
#51440=ORIENTED_EDGE ( 'NONE', *, *, #66540, .F. ) ;
#51593=ORIENTED_EDGE ( 'NONE', *, *, #17168, .F. ) ;
#51598=CIRCLE ( 'NONE', #73211, 12.49999999999999645 ) ;
#51638=EDGE_CURVE ( 'NONE', #16639, #986, #44841, .T. ) ;
#51663=CARTESIAN_POINT ( 'NONE',  ( 12.49999999999999645, 1.530808498934191127E-15, 125.0000000000000000 ) ) ;
#51682=EDGE_LOOP ( 'NONE', ( #13510, #63720, #2439, #12012, #11084, #32440 ) ) ;
#51934=PRESENTATION_STYLE_ASSIGNMENT (( #13191 ) ) ;
#51968=AXIS2_PLACEMENT_3D ( 'NONE', #60342, #25384, #8825 ) ;
#51992=ORIENTED_EDGE ( 'NONE', *, *, #67721, .F. ) ;
#52091=DIRECTION ( 'NONE',  ( -0.6575728627325955200, 0.7533909544171997208, 0.000000000000000000 ) ) ;
#52101=EDGE_CURVE ( 'NONE', #57864, #61855, #11790, .T. ) ;
#52116=ORIENTED_EDGE ( 'NONE', *, *, #17007, .T. ) ;
#52207=CYLINDRICAL_SURFACE ( 'NONE', #53962, 12.49999999999999645 ) ;
#52329=CARTESIAN_POINT ( 'NONE',  ( -12.49999999999999645, 0.000000000000000000, -44.99999999999998579 ) ) ;
#52358=LINE ( 'NONE', #17047, #3157 ) ;
#52414=DIRECTION ( 'NONE',  ( -0.000000000000000000, -0.000000000000000000, -1.000000000000000000 ) ) ;
#52496=DIRECTION ( 'NONE',  ( -1.000000000000000000, 0.000000000000000000, 0.000000000000000000 ) ) ;
#52511=CARTESIAN_POINT ( 'NONE',  ( 0.000000000000000000, 0.000000000000000000, 52.00000000000002132 ) ) ;
#52588=DIRECTION ( 'NONE',  ( 0.6575728627325957421, -0.7533909544171993877, -1.230411769795008318E-16 ) ) ;
#52609=EDGE_CURVE ( 'NONE', #50553, #36680, #25950, .T. ) ;
#52642=ORIENTED_EDGE ( 'NONE', *, *, #21212, .F. ) ;
#52652=DIRECTION ( 'NONE',  ( 0.000000000000000000, -0.000000000000000000, -1.000000000000000000 ) ) ;
#52675=SURFACE_STYLE_FILL_AREA ( #12445 ) ;
#52703=DIRECTION ( 'NONE',  ( -0.000000000000000000, -0.000000000000000000, -1.000000000000000000 ) ) ;
#52713=ORIENTED_EDGE ( 'NONE', *, *, #11003, .T. ) ;
#52762=DIRECTION ( 'NONE',  ( -0.000000000000000000, -0.000000000000000000, -1.000000000000000000 ) ) ;
#52786=EDGE_CURVE ( 'NONE', #48148, #39717, #63055, .T. ) ;
#52896=CARTESIAN_POINT ( 'NONE',  ( -12.49999999999999645, 0.000000000000000000, 125.0000000000000000 ) ) ;
#52996=CARTESIAN_POINT ( 'NONE',  ( 0.000000000000000000, 0.000000000000000000, 53.20000000000001705 ) ) ;
#53002=EDGE_CURVE ( 'NONE', #63923, #68344, #652, .T. ) ;
#53018=CIRCLE ( 'NONE', #47008, 12.49999999999999645 ) ;
#53035=DIRECTION ( 'NONE',  ( 1.000000000000000000, 0.000000000000000000, 0.000000000000000000 ) ) ;
#53086=ORIENTED_EDGE ( 'NONE', *, *, #50319, .T. ) ;
#53101=ORIENTED_EDGE ( 'NONE', *, *, #47763, .F. ) ;
#53426=CARTESIAN_POINT ( 'NONE',  ( 0.000000000000000000, 0.000000000000000000, 42.00000000000001421 ) ) ;
#53481=CARTESIAN_POINT ( 'NONE',  ( 0.000000000000000000, 0.000000000000000000, 125.0000000000000000 ) ) ;
#53543=ORIENTED_EDGE ( 'NONE', *, *, #9319, .F. ) ;
#53586=DIRECTION ( 'NONE',  ( 0.000000000000000000, 0.000000000000000000, -1.000000000000000000 ) ) ;
#53673=DIRECTION ( 'NONE',  ( 0.000000000000000000, 0.000000000000000000, 1.000000000000000000 ) ) ;
#53884=EDGE_CURVE ( 'NONE', #48148, #48900, #58432, .T. ) ;
#53962=AXIS2_PLACEMENT_3D ( 'NONE', #69861, #11602, #57861 ) ;
#53997=ADVANCED_FACE ( 'NONE', ( #2812 ), #54288, .F. ) ;
#54075=LINE ( 'NONE', #58593, #59494 ) ;
#54095=ORIENTED_EDGE ( 'NONE', *, *, #54343, .F. ) ;
#54171=STYLED_ITEM ( 'NONE', ( #203 ), #7701 ) ;
#54175=EDGE_CURVE ( 'NONE', #35072, #54619, #45612, .T. ) ;
#54218=ORIENTED_EDGE ( 'NONE', *, *, #7331, .F. ) ;
#54235=CARTESIAN_POINT ( 'NONE',  ( -8.637688417678527131, 13.69818742750669394, 52.00000000000002132 ) ) ;
#54246=ADVANCED_FACE ( 'NONE', ( #64641 ), #31159, .T. ) ;
#54288=PLANE ( 'NONE',  #17649 ) ;
#54315=CARTESIAN_POINT ( 'NONE',  ( -12.49999999999999645, 0.000000000000000000, 42.00000000000001421 ) ) ;
#54323=FACE_OUTER_BOUND ( 'NONE', #45740, .T. ) ;
#54330=DIRECTION ( 'NONE',  ( 1.000000000000000000, 0.000000000000000000, 0.000000000000000000 ) ) ;
#54343=EDGE_CURVE ( 'NONE', #45782, #16094, #20108, .T. ) ;
#54347=ORIENTED_EDGE ( 'NONE', *, *, #37772, .F. ) ;
#54377=CARTESIAN_POINT ( 'NONE',  ( 0.000000000000000000, 0.000000000000000000, -56.19999999999998863 ) ) ;
#54437=DIRECTION ( 'NONE',  ( -1.000000000000000000, 0.000000000000000000, 0.000000000000000000 ) ) ;
#54447=EDGE_LOOP ( 'NONE', ( #66959, #33016, #37352, #4771, #55656, #63806 ) ) ;
#54550=CARTESIAN_POINT ( 'NONE',  ( -12.40464318976452596, 10.41032311384371489, 42.00000000000001421 ) ) ;
#54596=ADVANCED_FACE ( 'NONE', ( #39784, #5213 ), #33758, .T. ) ;
#54619=VERTEX_POINT ( 'NONE', #22490 ) ;
#54660=VECTOR ( 'NONE', #27779, 1000.000000000000000 ) ;
#54684=DIRECTION ( 'NONE',  ( 0.000000000000000000, 0.000000000000000000, 1.000000000000000000 ) ) ;
#54702=FACE_OUTER_BOUND ( 'NONE', #36776, .T. ) ;
#54865=EDGE_CURVE ( 'NONE', #68424, #16094, #8889, .T. ) ;
#54978=ORIENTED_EDGE ( 'NONE', *, *, #11716, .T. ) ;
#55031=UNCERTAINTY_MEASURE_WITH_UNIT (LENGTH_MEASURE( 1.000000000000000082E-05 ), #38147, 'distance_accuracy_value', 'NONE');
#55158=FACE_OUTER_BOUND ( 'NONE', #56533, .T. ) ;
#55160=CARTESIAN_POINT ( 'NONE',  ( -11.59999999999999787, 0.000000000000000000, -44.99999999999998579 ) ) ;
#55186=ADVANCED_FACE ( 'NONE', ( #69364 ), #1364, .F. ) ;
#55191=CIRCLE ( 'NONE', #56451, 11.59999999999999787 ) ;
#55261=DIRECTION ( 'NONE',  ( -1.000000000000000000, 0.000000000000000000, 0.000000000000000000 ) ) ;
#55318=FACE_OUTER_BOUND ( 'NONE', #28949, .T. ) ;
#55323=DIRECTION ( 'NONE',  ( 0.000000000000000000, 0.000000000000000000, -1.000000000000000000 ) ) ;
#55479=ORIENTED_EDGE ( 'NONE', *, *, #67553, .F. ) ;
#55596=ORIENTED_EDGE ( 'NONE', *, *, #12246, .T. ) ;
#55635=DIRECTION ( 'NONE',  ( 0.6575728627325957421, -0.7533909544171993877, -1.230411769795008318E-16 ) ) ;
#55649=ADVANCED_FACE ( 'NONE', ( #22988 ), #22235, .T. ) ;
#55656=ORIENTED_EDGE ( 'NONE', *, *, #63705, .F. ) ;
#55701=VERTEX_POINT ( 'NONE', #41379 ) ;
#55744=DIRECTION ( 'NONE',  ( -0.000000000000000000, -0.000000000000000000, -1.000000000000000000 ) ) ;
#55791=ADVANCED_FACE ( 'NONE', ( #48495 ), #64315, .F. ) ;
#55814=SURFACE_SIDE_STYLE ('',( #5444 ) ) ;
#55852=ORIENTED_EDGE ( 'NONE', *, *, #62151, .T. ) ;
#55861=LINE ( 'NONE', #61507, #7964 ) ;
#55869=ORIENTED_EDGE ( 'NONE', *, *, #47196, .F. ) ;
#56140=DIRECTION ( 'NONE',  ( -0.000000000000000000, -0.000000000000000000, -1.000000000000000000 ) ) ;
#56171=CARTESIAN_POINT ( 'NONE',  ( 0.000000000000000000, 0.000000000000000000, 125.0000000000000000 ) ) ;
#56216=ADVANCED_FACE ( 'NONE', ( #70573 ), #31106, .T. ) ;
#56251=DIRECTION ( 'NONE',  ( 0.000000000000000000, 0.000000000000000000, 1.000000000000000000 ) ) ;
#56269=CARTESIAN_POINT ( 'NONE',  ( -7.469491406282094736, 4.756046723998911929, 42.00000000000001421 ) ) ;
#56331=DIRECTION ( 'NONE',  ( 1.000000000000000000, 0.000000000000000000, -0.000000000000000000 ) ) ;
#56451=AXIS2_PLACEMENT_3D ( 'NONE', #41277, #19069, #70193 ) ;
#56460=CARTESIAN_POINT ( 'NONE',  ( 0.000000000000000000, 0.000000000000000000, 125.0000000000000000 ) ) ;
#56533=EDGE_LOOP ( 'NONE', ( #48761, #17201, #62645, #72296, #60458, #39208, #66837, #939 ) ) ;
#56555=CARTESIAN_POINT ( 'NONE',  ( -6.782329983125267248, 10.49999999999999645, -104.9999999999999858 ) ) ;
#56606=ORIENTED_EDGE ( 'NONE', *, *, #24694, .F. ) ;
#56670=ORIENTED_EDGE ( 'NONE', *, *, #9347, .T. ) ;
#56838=PLANE ( 'NONE',  #62286 ) ;
#56852=CARTESIAN_POINT ( 'NONE',  ( 12.49999999999999645, 1.530808498934191127E-15, -56.19999999999998863 ) ) ;
#56889=ORIENTED_EDGE ( 'NONE', *, *, #7331, .T. ) ;
#57026=AXIS2_PLACEMENT_3D ( 'NONE', #15036, #72900, #21790 ) ;
#57132=LINE ( 'NONE', #45112, #16625 ) ;
#57169=ORIENTED_EDGE ( 'NONE', *, *, #69406, .F. ) ;
#57271=DIRECTION ( 'NONE',  ( 0.000000000000000000, 0.000000000000000000, -1.000000000000000000 ) ) ;
#57300=SURFACE_STYLE_USAGE ( .BOTH. , #55814 ) ;
#57307=DIRECTION ( 'NONE',  ( -0.000000000000000000, -0.000000000000000000, -1.000000000000000000 ) ) ;
#57377=ORIENTED_EDGE ( 'NONE', *, *, #40131, .F. ) ;
#57525=ORIENTED_EDGE ( 'NONE', *, *, #14946, .F. ) ;
#57558=CARTESIAN_POINT ( 'NONE',  ( 0.000000000000000000, 0.000000000000000000, 42.00000000000001421 ) ) ;
#57702=ORIENTED_EDGE ( 'NONE', *, *, #47118, .F. ) ;
#57812=CARTESIAN_POINT ( 'NONE',  ( 0.000000000000000000, 0.000000000000000000, 40.80000000000001847 ) ) ;
#57822=( GEOMETRIC_REPRESENTATION_CONTEXT ( 3 ) GLOBAL_UNCERTAINTY_ASSIGNED_CONTEXT ( ( #61049 ) ) GLOBAL_UNIT_ASSIGNED_CONTEXT ( ( #33615, #44543, #39272 ) ) REPRESENTATION_CONTEXT ( 'NONE', 'WORKASPACE' ) );
#57841=ORIENTED_EDGE ( 'NONE', *, *, #50061, .F. ) ;
#57861=DIRECTION ( 'NONE',  ( -1.000000000000000000, 0.000000000000000000, 0.000000000000000000 ) ) ;
#57864=VERTEX_POINT ( 'NONE', #60283 ) ;
#57953=( LENGTH_UNIT ( ) NAMED_UNIT ( * ) SI_UNIT ( .MILLI., .METRE. ) );
#58054=VERTEX_POINT ( 'NONE', #46953 ) ;
#58150=CARTESIAN_POINT ( 'NONE',  ( 0.000000000000000000, 0.000000000000000000, 52.00000000000002132 ) ) ;
#58161=ORIENTED_EDGE ( 'NONE', *, *, #11003, .F. ) ;
#58186=VERTEX_POINT ( 'NONE', #7830 ) ;
#58188=CARTESIAN_POINT ( 'NONE',  ( 0.000000000000000000, 0.000000000000000000, -54.99999999999998579 ) ) ;
#58215=EDGE_CURVE ( 'NONE', #58186, #63730, #54075, .T. ) ;
#58260=ORIENTED_EDGE ( 'NONE', *, *, #7902, .T. ) ;
#58269=DIRECTION ( 'NONE',  ( 0.000000000000000000, 0.000000000000000000, 1.000000000000000000 ) ) ;
#58320=( NAMED_UNIT ( * ) SI_UNIT ( $, .STERADIAN. ) SOLID_ANGLE_UNIT ( ) );
#58327=DIRECTION ( 'NONE',  ( 1.000000000000000000, 0.000000000000000000, 0.000000000000000000 ) ) ;
#58378=LINE ( 'NONE', #6877, #58689 ) ;
#58421=ORIENTED_EDGE ( 'NONE', *, *, #27582, .T. ) ;
#58432=LINE ( 'NONE', #6926, #32067 ) ;
#58533=AXIS2_PLACEMENT_3D ( 'NONE', #52996, #18394, #24413 ) ;
#58553=DIRECTION ( 'NONE',  ( 1.000000000000000000, 0.000000000000000000, 0.000000000000000000 ) ) ;
#58592=MECHANICAL_DESIGN_GEOMETRIC_PRESENTATION_REPRESENTATION('',(#32177),#69428);
#58593=CARTESIAN_POINT ( 'NONE',  ( -8.637688417678527131, 13.69818742750669394, 42.00000000000001421 ) ) ;
#58623=CARTESIAN_POINT ( 'NONE',  ( 0.000000000000000000, 0.000000000000000000, 42.00000000000001421 ) ) ;
#58668=CARTESIAN_POINT ( 'NONE',  ( 0.000000000000000000, 0.000000000000000000, -125.0000000000000000 ) ) ;
#58689=VECTOR ( 'NONE', #18519, 1000.000000000000000 ) ;
#58741=DIRECTION ( 'NONE',  ( 1.000000000000000000, 0.000000000000000000, 0.000000000000000000 ) ) ;
#58950=VERTEX_POINT ( 'NONE', #59564 ) ;
#58951=VECTOR ( 'NONE', #38986, 1000.000000000000000 ) ;
#58977=DIRECTION ( 'NONE',  ( 1.000000000000000000, 0.000000000000000000, 0.000000000000000000 ) ) ;
#58985=ORIENTED_EDGE ( 'NONE', *, *, #9347, .F. ) ;
#58996=EDGE_LOOP ( 'NONE', ( #4187, #60815, #63860, #29112 ) ) ;
#59078=ORIENTED_EDGE ( 'NONE', *, *, #37772, .T. ) ;
#59095=EDGE_LOOP ( 'NONE', ( #34557, #25031, #50018, #37568, #20685, #54218 ) ) ;
#59168=AXIS2_PLACEMENT_3D ( 'NONE', #27901, #43735, #60654 ) ;
#59375=ORIENTED_EDGE ( 'NONE', *, *, #12716, .F. ) ;
#59420=AXIS2_PLACEMENT_3D ( 'NONE', #46154, #1068, #69086 ) ;
#59494=VECTOR ( 'NONE', #2611, 1000.000000000000000 ) ;
#59564=CARTESIAN_POINT ( 'NONE',  ( 11.59999999999999787, 1.420590287010929336E-15, 40.80000000000001847 ) ) ;
#59591=DIRECTION ( 'NONE',  ( 1.000000000000000000, 0.000000000000000000, 0.000000000000000000 ) ) ;
#59723=FACE_OUTER_BOUND ( 'NONE', #30378, .T. ) ;
#59823=ORIENTED_EDGE ( 'NONE', *, *, #48628, .F. ) ;
#59913=AXIS2_PLACEMENT_3D ( 'NONE', #30153, #18501, #58741 ) ;
#59980=DIRECTION ( 'NONE',  ( 1.000000000000000000, 0.000000000000000000, 0.000000000000000000 ) ) ;
#59990=CARTESIAN_POINT ( 'NONE',  ( -7.469491406282094736, 4.756046723998911929, 42.00000000000001421 ) ) ;
#60098=DIRECTION ( 'NONE',  ( 0.000000000000000000, 0.000000000000000000, -1.000000000000000000 ) ) ;
#60118=ORIENTED_EDGE ( 'NONE', *, *, #26535, .F. ) ;
#60212=EDGE_LOOP ( 'NONE', ( #20835, #39676, #59078, #31145, #73957, #58985, #21145, #3815 ) ) ;
#60283=CARTESIAN_POINT ( 'NONE',  ( 12.49999999999999645, 1.530808498934191127E-15, 52.00000000000002132 ) ) ;
#60334=DIRECTION ( 'NONE',  ( -1.000000000000000000, 0.000000000000000000, 0.000000000000000000 ) ) ;
#60342=CARTESIAN_POINT ( 'NONE',  ( 0.000000000000000000, 0.000000000000000000, -44.99999999999998579 ) ) ;
#60350=EDGE_CURVE ( 'NONE', #1809, #71558, #65973, .T. ) ;
#60361=CIRCLE ( 'NONE', #14664, 11.59999999999999787 ) ;
#60434=ADVANCED_FACE ( 'NONE', ( #27578 ), #21941, .F. ) ;
#60458=ORIENTED_EDGE ( 'NONE', *, *, #14410, .T. ) ;
#60462=FACE_OUTER_BOUND ( 'NONE', #51682, .T. ) ;
#60464=VECTOR ( 'NONE', #33704, 1000.000000000000114 ) ;
#60473=DIRECTION ( 'NONE',  ( 0.7533909544171998318, 0.6575728627325954090, 0.000000000000000000 ) ) ;
#60504=EDGE_LOOP ( 'NONE', ( #32058, #55479, #63815, #63566 ) ) ;
#60593=ORIENTED_EDGE ( 'NONE', *, *, #718, .T. ) ;
#60614=AXIS2_PLACEMENT_3D ( 'NONE', #61966, #16465, #49921 ) ;
#60654=DIRECTION ( 'NONE',  ( 1.000000000000000000, 0.000000000000000000, 0.000000000000000000 ) ) ;
#60659=EDGE_LOOP ( 'NONE', ( #49104, #64821, #67773, #52642, #1108, #68541 ) ) ;
#60660=ORIENTED_EDGE ( 'NONE', *, *, #26535, .T. ) ;
#60701=EDGE_CURVE ( 'NONE', #45793, #41715, #52358, .T. ) ;
#60723=CARTESIAN_POINT ( 'NONE',  ( -3.702536634196121224, 8.043911037661892749, -64.01812422950395387 ) ) ;
#60815=ORIENTED_EDGE ( 'NONE', *, *, #69033, .F. ) ;
#60901=CIRCLE ( 'NONE', #64500, 11.59999999999999787 ) ;
#61028=EDGE_LOOP ( 'NONE', ( #8595, #25255, #71715, #34671, #74047, #45692, #67784, #15368 ) ) ;
#61049=UNCERTAINTY_MEASURE_WITH_UNIT (LENGTH_MEASURE( 1.000000000000000082E-05 ), #33615, 'distance_accuracy_value', 'NONE');
#61101=ORIENTED_EDGE ( 'NONE', *, *, #28341, .F. ) ;
#61121=CIRCLE ( 'NONE', #43098, 11.59999999999999787 ) ;
#61197=EDGE_CURVE ( 'NONE', #65205, #26530, #28397, .T. ) ;
#61236=ORIENTED_EDGE ( 'NONE', *, *, #32765, .T. ) ;
#61254=ORIENTED_EDGE ( 'NONE', *, *, #61197, .F. ) ;
#61261=LINE ( 'NONE', #44717, #54660 ) ;
#61282=DIRECTION ( 'NONE',  ( 0.000000000000000000, 0.000000000000000000, 1.000000000000000000 ) ) ;
#61323=AXIS2_PLACEMENT_3D ( 'NONE', #40637, #39530, #18075 ) ;
#61462=SHAPE_REPRESENTATION_RELATIONSHIP ( 'NONE' , 'NONE' ,  #8524, #7701 ) ;
#61479=VECTOR ( 'NONE', #9915, 1000.000000000000114 ) ;
#61507=CARTESIAN_POINT ( 'NONE',  ( -7.469491406282116941, 4.756046723998916370, -55.00000000000000000 ) ) ;
#61588=AXIS2_PLACEMENT_3D ( 'NONE', #24736, #13809, #48039 ) ;
#61660=CARTESIAN_POINT ( 'NONE',  ( -8.637688417678527131, 13.69818742750669394, 32.98187577049606745 ) ) ;
#61855=VERTEX_POINT ( 'NONE', #33308 ) ;
#61883=ORIENTED_EDGE ( 'NONE', *, *, #47118, .T. ) ;
#61966=CARTESIAN_POINT ( 'NONE',  ( -1.895993822078342774E-14, 1.063390998062931622E-14, -55.00000000000000000 ) ) ;
#62084=CYLINDRICAL_SURFACE ( 'NONE', #38605, 12.49999999999999645 ) ;
#62134=EDGE_LOOP ( 'NONE', ( #54347, #61236, #26213, #60118, #9729, #13305 ) ) ;
#62151=EDGE_CURVE ( 'NONE', #19511, #68424, #8166, .T. ) ;
#62186=DIRECTION ( 'NONE',  ( 1.000000000000000000, 0.000000000000000000, 0.000000000000000000 ) ) ;
#62244=DIRECTION ( 'NONE',  ( -0.000000000000000000, -0.000000000000000000, -1.000000000000000000 ) ) ;
#62286=AXIS2_PLACEMENT_3D ( 'NONE', #10583, #3230, #5346 ) ;
#62331=LINE ( 'NONE', #72826, #36305 ) ;
#62456=VERTEX_POINT ( 'NONE', #73217 ) ;
#62470=EDGE_CURVE ( 'NONE', #27241, #66920, #22102, .T. ) ;
#62559=EDGE_CURVE ( 'NONE', #14320, #25862, #18302, .T. ) ;
#62582=CARTESIAN_POINT ( 'NONE',  ( -3.702536634196119447, 8.043911037661890973, -45.00000000000000000 ) ) ;
#62584=DIRECTION ( 'NONE',  ( 1.000000000000000000, 0.000000000000000000, 0.000000000000000000 ) ) ;
#62644=AXIS2_PLACEMENT_3D ( 'NONE', #43268, #26677, #55261 ) ;
#62645=ORIENTED_EDGE ( 'NONE', *, *, #8076, .T. ) ;
#62653=FACE_OUTER_BOUND ( 'NONE', #31040, .T. ) ;
#62674=DIRECTION ( 'NONE',  ( -0.7533909544171997208, -0.6575728627325955200, 0.000000000000000000 ) ) ;
#62779=CARTESIAN_POINT ( 'NONE',  ( -11.59999999999999787, 0.000000000000000000, -56.19999999999998863 ) ) ;
#62818=DIRECTION ( 'NONE',  ( 1.000000000000000000, 0.000000000000000000, 0.000000000000000000 ) ) ;
#62860=EDGE_CURVE ( 'NONE', #65693, #47656, #26898, .T. ) ;
#63055=CIRCLE ( 'NONE', #57026, 12.49999999999999645 ) ;
#63177=ORIENTED_EDGE ( 'NONE', *, *, #25557, .T. ) ;
#63211=CARTESIAN_POINT ( 'NONE',  ( 0.000000000000000000, 0.000000000000000000, 125.0000000000000000 ) ) ;
#63312=CARTESIAN_POINT ( 'NONE',  ( 0.000000000000000000, 0.000000000000000000, 125.0000000000000000 ) ) ;
#63404=LINE ( 'NONE', #28431, #58951 ) ;
#63554=CARTESIAN_POINT ( 'NONE',  ( 0.000000000000000000, 0.000000000000000000, -54.99999999999998579 ) ) ;
#63566=ORIENTED_EDGE ( 'NONE', *, *, #44433, .T. ) ;
#63585=AXIS2_PLACEMENT_3D ( 'NONE', #1500, #47684, #58977 ) ;
#63595=VECTOR ( 'NONE', #18781, 1000.000000000000114 ) ;
#63652=PLANE ( 'NONE',  #30749 ) ;
#63705=EDGE_CURVE ( 'NONE', #70313, #62456, #63937, .T. ) ;
#63720=ORIENTED_EDGE ( 'NONE', *, *, #60701, .T. ) ;
#63730=VERTEX_POINT ( 'NONE', #22978 ) ;
#63742=DIRECTION ( 'NONE',  ( 0.000000000000000000, -0.000000000000000000, 1.000000000000000000 ) ) ;
#63790=DIRECTION ( 'NONE',  ( 0.000000000000000000, 0.000000000000000000, 1.000000000000000000 ) ) ;
#63806=ORIENTED_EDGE ( 'NONE', *, *, #7902, .F. ) ;
#63815=ORIENTED_EDGE ( 'NONE', *, *, #17168, .T. ) ;
#63860=ORIENTED_EDGE ( 'NONE', *, *, #60350, .F. ) ;
#63908=DIRECTION ( 'NONE',  ( 0.000000000000000000, 0.000000000000000000, 1.000000000000000000 ) ) ;
#63923=VERTEX_POINT ( 'NONE', #25182 ) ;
#63937=LINE ( 'NONE', #17691, #70722 ) ;
#63965=AXIS2_PLACEMENT_3D ( 'NONE', #46279, #68851, #12427 ) ;
#64213=ORIENTED_EDGE ( 'NONE', *, *, #62860, .T. ) ;
#64261=FACE_OUTER_BOUND ( 'NONE', #60212, .T. ) ;
#64315=PLANE ( 'NONE',  #8732 ) ;
#64356=CARTESIAN_POINT ( 'NONE',  ( 11.59999999999999787, 1.420590287010929336E-15, 42.00000000000001421 ) ) ;
#64366=ORIENTED_EDGE ( 'NONE', *, *, #60350, .T. ) ;
#64500=AXIS2_PLACEMENT_3D ( 'NONE', #58150, #69069, #41229 ) ;
#64525=FACE_OUTER_BOUND ( 'NONE', #45604, .T. ) ;
#64579=AXIS2_PLACEMENT_3D ( 'NONE', #3307, #37133, #14555 ) ;
#64601=LINE ( 'NONE', #30741, #43180 ) ;
#64641=FACE_OUTER_BOUND ( 'NONE', #27444, .T. ) ;
#64710=DIRECTION ( 'NONE',  ( 0.6575728627325954090, -0.7533909544171998318, 0.000000000000000000 ) ) ;
#64767=EDGE_CURVE ( 'NONE', #55701, #25862, #2354, .T. ) ;
#64821=ORIENTED_EDGE ( 'NONE', *, *, #9319, .T. ) ;
#64835=EDGE_LOOP ( 'NONE', ( #35139, #22777, #53086, #72473 ) ) ;
#64880=CARTESIAN_POINT ( 'NONE',  ( -6.782329983125267248, 10.49999999999999645, -105.0000000000000000 ) ) ;
#64943=CARTESIAN_POINT ( 'NONE',  ( -9.332068499558245023, 6.890028847512374988, 52.00000000000002132 ) ) ;
#64949=DIRECTION ( 'NONE',  ( 1.000000000000000000, 0.000000000000000000, 0.000000000000000000 ) ) ;
#65163=CARTESIAN_POINT ( 'NONE',  ( -9.332068499558252128, 6.890028847512362553, -44.99999999999998579 ) ) ;
#65205=VERTEX_POINT ( 'NONE', #34597 ) ;
#65301=DIRECTION ( 'NONE',  ( 0.000000000000000000, 0.000000000000000000, 1.000000000000000000 ) ) ;
#65371=DIRECTION ( 'NONE',  ( -0.7533909544171994987, -0.6575728627325958531, 2.465190328815662439E-32 ) ) ;
#65408=ORIENTED_EDGE ( 'NONE', *, *, #38618, .F. ) ;
#65413=ORIENTED_EDGE ( 'NONE', *, *, #40131, .T. ) ;
#65426=CARTESIAN_POINT ( 'NONE',  ( -9.937067298023311679, 7.583184918921313411, 125.0000000000000000 ) ) ;
#65441=CIRCLE ( 'NONE', #59420, 11.59999999999999787 ) ;
#65603=DIRECTION ( 'NONE',  ( 0.000000000000000000, 0.000000000000000000, 1.000000000000000000 ) ) ;
#65612=EDGE_CURVE ( 'NONE', #58054, #2275, #44587, .T. ) ;
#65613=DIRECTION ( 'NONE',  ( 0.000000000000000000, 0.000000000000000000, 1.000000000000000000 ) ) ;
#65693=VERTEX_POINT ( 'NONE', #46919 ) ;
#65791=AXIS2_PLACEMENT_3D ( 'NONE', #39921, #11685, #23000 ) ;
#65928=ORIENTED_EDGE ( 'NONE', *, *, #49056, .T. ) ;
#65973=LINE ( 'NONE', #24985, #21090 ) ;
#65977=VERTEX_POINT ( 'NONE', #22320 ) ;
#66067=DIRECTION ( 'NONE',  ( -1.000000000000000000, 0.000000000000000000, 0.000000000000000000 ) ) ;
#66074=ADVANCED_FACE ( 'NONE', ( #18883 ), #1290, .T. ) ;
#66097=VECTOR ( 'NONE', #53586, 1000.000000000000000 ) ;
#66233=EDGE_LOOP ( 'NONE', ( #40466, #55869, #57169, #30904 ) ) ;
#66265=ORIENTED_EDGE ( 'NONE', *, *, #15006, .F. ) ;
#66267=AXIS2_PLACEMENT_3D ( 'NONE', #32380, #55323, #15847 ) ;
#66273=DIRECTION ( 'NONE',  ( 0.000000000000000000, -0.000000000000000000, 1.000000000000000000 ) ) ;
#66316=ORIENTED_EDGE ( 'NONE', *, *, #52609, .T. ) ;
#66350=FACE_BOUND ( 'NONE', #8425, .T. ) ;
#66476=ADVANCED_FACE ( 'NONE', ( #21853 ), #40262, .T. ) ;
#66522=VECTOR ( 'NONE', #57307, 1000.000000000000000 ) ;
#66540=EDGE_CURVE ( 'NONE', #32702, #2275, #36096, .T. ) ;
#66765=DIRECTION ( 'NONE',  ( 0.000000000000000000, 0.000000000000000000, -1.000000000000000000 ) ) ;
#66791=EDGE_CURVE ( 'NONE', #5740, #71004, #25551, .T. ) ;
#66837=ORIENTED_EDGE ( 'NONE', *, *, #22395, .F. ) ;
#66868=EDGE_CURVE ( 'NONE', #1281, #73677, #61261, .T. ) ;
#66875=ORIENTED_EDGE ( 'NONE', *, *, #63705, .T. ) ;
#66887=AXIS2_PLACEMENT_3D ( 'NONE', #29696, #25188, #7529 ) ;
#66920=VERTEX_POINT ( 'NONE', #16129 ) ;
#66959=ORIENTED_EDGE ( 'NONE', *, *, #30223, .T. ) ;
#66991=DIRECTION ( 'NONE',  ( 0.000000000000000000, 0.000000000000000000, 1.000000000000000000 ) ) ;
#67017=ORIENTED_EDGE ( 'NONE', *, *, #37163, .T. ) ;
#67229=CIRCLE ( 'NONE', #44370, 12.49999999999999645 ) ;
#67286=DIRECTION ( 'NONE',  ( 1.000000000000000000, 0.000000000000000000, 0.000000000000000000 ) ) ;
#67372=LINE ( 'NONE', #11336, #29758 ) ;
#67376=EDGE_CURVE ( 'NONE', #7618, #50553, #73172, .T. ) ;
#67437=DIRECTION ( 'NONE',  ( 0.7533909544171997208, 0.6575728627325955200, 0.000000000000000000 ) ) ;
#67488=CARTESIAN_POINT ( 'NONE',  ( -7.469491406282116941, 4.756046723998916370, -55.00000000000000000 ) ) ;
#67551=LINE ( 'NONE', #27696, #60464 ) ;
#67553=EDGE_CURVE ( 'NONE', #65977, #27241, #30658, .T. ) ;
#67618=ORIENTED_EDGE ( 'NONE', *, *, #11716, .F. ) ;
#67721=EDGE_CURVE ( 'NONE', #21877, #58950, #17526, .T. ) ;
#67728=FACE_OUTER_BOUND ( 'NONE', #24269, .T. ) ;
#67734=DIRECTION ( 'NONE',  ( 1.000000000000000000, 0.000000000000000000, 0.000000000000000000 ) ) ;
#67758=EDGE_CURVE ( 'NONE', #7618, #37316, #2855, .T. ) ;
#67773=ORIENTED_EDGE ( 'NONE', *, *, #53002, .T. ) ;
#67784=ORIENTED_EDGE ( 'NONE', *, *, #64767, .T. ) ;
#67822=CARTESIAN_POINT ( 'NONE',  ( -11.59999999999999787, 0.000000000000000000, 40.80000000000001847 ) ) ;
#68021=ADVANCED_FACE ( 'NONE', ( #29435 ), #927, .T. ) ;
#68041=DIRECTION ( 'NONE',  ( -0.6575728627325954090, 0.7533909544171998318, 0.000000000000000000 ) ) ;
#68076=DIRECTION ( 'NONE',  ( 0.000000000000000000, 0.000000000000000000, 1.000000000000000000 ) ) ;
#68207=CARTESIAN_POINT ( 'NONE',  ( -8.637688417678548447, 13.69818742750669571, -45.00000000000000000 ) ) ;
#68231=AXIS2_PLACEMENT_3D ( 'NONE', #24738, #47666, #70575 ) ;
#68344=VERTEX_POINT ( 'NONE', #62779 ) ;
#68347=CIRCLE ( 'NONE', #41941, 12.49999999999999645 ) ;
#68419=DIRECTION ( 'NONE',  ( 1.000000000000000000, 0.000000000000000000, 0.000000000000000000 ) ) ;
#68424=VERTEX_POINT ( 'NONE', #14140 ) ;
#68502=EDGE_CURVE ( 'NONE', #54619, #32157, #55861, .T. ) ;
#68541=ORIENTED_EDGE ( 'NONE', *, *, #37163, .F. ) ;
#68574=CARTESIAN_POINT ( 'NONE',  ( 0.000000000000000000, 0.000000000000000000, 125.0000000000000000 ) ) ;
#68645=ORIENTED_EDGE ( 'NONE', *, *, #74018, .F. ) ;
#68705=ORIENTED_EDGE ( 'NONE', *, *, #13179, .T. ) ;
#68750=DIRECTION ( 'NONE',  ( 0.000000000000000000, 0.000000000000000000, 1.000000000000000000 ) ) ;
#68851=DIRECTION ( 'NONE',  ( 0.000000000000000000, 0.000000000000000000, -1.000000000000000000 ) ) ;
#68881=DIRECTION ( 'NONE',  ( 1.000000000000000000, 0.000000000000000000, 0.000000000000000000 ) ) ;
#68886=CIRCLE ( 'NONE', #5261, 11.59999999999999787 ) ;
#69033=EDGE_CURVE ( 'NONE', #71558, #55701, #17890, .T. ) ;
#69069=DIRECTION ( 'NONE',  ( 0.000000000000000000, 0.000000000000000000, 1.000000000000000000 ) ) ;
#69086=DIRECTION ( 'NONE',  ( 1.000000000000000000, 0.000000000000000000, 0.000000000000000000 ) ) ;
#69171=UNCERTAINTY_MEASURE_WITH_UNIT (LENGTH_MEASURE( 1.000000000000000082E-05 ), #57953, 'distance_accuracy_value', 'NONE');
#69210=DIRECTION ( 'NONE',  ( -1.000000000000000000, 0.000000000000000000, 0.000000000000000000 ) ) ;
#69220=ORIENTED_EDGE ( 'NONE', *, *, #44849, .F. ) ;
#69229=CARTESIAN_POINT ( 'NONE',  ( 6.782329983125267248, 10.49999999999999645, -105.0000000000000000 ) ) ;
#69364=FACE_OUTER_BOUND ( 'NONE', #45369, .T. ) ;
#69406=EDGE_CURVE ( 'NONE', #42737, #62456, #16702, .T. ) ;
#69428=( GEOMETRIC_REPRESENTATION_CONTEXT ( 3 ) GLOBAL_UNCERTAINTY_ASSIGNED_CONTEXT ( ( #69171 ) ) GLOBAL_UNIT_ASSIGNED_CONTEXT ( ( #57953, #30471, #58320 ) ) REPRESENTATION_CONTEXT ( 'NONE', 'WORKASPACE' ) );
#69454=VECTOR ( 'NONE', #6660, 1000.000000000000000 ) ;
#69669=DIRECTION ( 'NONE',  ( 1.000000000000000000, 0.000000000000000000, 0.000000000000000000 ) ) ;
#69861=CARTESIAN_POINT ( 'NONE',  ( 0.000000000000000000, 0.000000000000000000, 125.0000000000000000 ) ) ;
#69879=CIRCLE ( 'NONE', #39915, 12.49999999999999645 ) ;
#69996=DIRECTION ( 'NONE',  ( -1.000000000000000000, 0.000000000000000000, 0.000000000000000000 ) ) ;
#70025=AXIS2_PLACEMENT_3D ( 'NONE', #32952, #15683, #14934 ) ;
#70185=CARTESIAN_POINT ( 'NONE',  ( -7.469491406282117829, 4.756046723998917258, -64.01812422950395387 ) ) ;
#70193=DIRECTION ( 'NONE',  ( 1.000000000000000000, 0.000000000000000000, 0.000000000000000000 ) ) ;
#70277=CARTESIAN_POINT ( 'NONE',  ( -12.40464318976454727, 10.41032311384371845, -55.00000000000000000 ) ) ;
#70309=AXIS2_PLACEMENT_3D ( 'NONE', #12245, #45749, #35913 ) ;
#70313=VERTEX_POINT ( 'NONE', #26033 ) ;
#70358=VECTOR ( 'NONE', #65613, 1000.000000000000000 ) ;
#70398=AXIS2_PLACEMENT_3D ( 'NONE', #57558, #6067, #46272 ) ;
#70511=ORIENTED_EDGE ( 'NONE', *, *, #22395, .T. ) ;
#70573=FACE_OUTER_BOUND ( 'NONE', #60659, .T. ) ;
#70575=DIRECTION ( 'NONE',  ( 1.000000000000000000, 0.000000000000000000, 0.000000000000000000 ) ) ;
#70604=CARTESIAN_POINT ( 'NONE',  ( -12.40464318976454905, 10.41032311384371845, -64.01812422950393966 ) ) ;
#70606=VECTOR ( 'NONE', #62244, 1000.000000000000000 ) ;
#70693=EDGE_LOOP ( 'NONE', ( #34676, #37341, #20096, #23399, #54978, #51593 ) ) ;
#70722=VECTOR ( 'NONE', #28221, 1000.000000000000114 ) ;
#70807=AXIS2_PLACEMENT_3D ( 'NONE', #7687, #19330, #13687 ) ;
#70820=ORIENTED_EDGE ( 'NONE', *, *, #1764, .F. ) ;
#71004=VERTEX_POINT ( 'NONE', #12723 ) ;
#71022=EDGE_CURVE ( 'NONE', #1974, #45793, #17891, .T. ) ;
#71103=DIRECTION ( 'NONE',  ( 0.000000000000000000, 0.000000000000000000, -1.000000000000000000 ) ) ;
#71205=CARTESIAN_POINT ( 'NONE',  ( 0.000000000000000000, 0.000000000000000000, 125.0000000000000000 ) ) ;
#71232=DIRECTION ( 'NONE',  ( 0.000000000000000000, 0.000000000000000000, 1.000000000000000000 ) ) ;
#71403=DIRECTION ( 'NONE',  ( -0.000000000000000000, -0.000000000000000000, -1.000000000000000000 ) ) ;
#71558=VERTEX_POINT ( 'NONE', #56555 ) ;
#71598=CARTESIAN_POINT ( 'NONE',  ( 0.000000000000000000, 0.000000000000000000, 52.00000000000002132 ) ) ;
#71659=DIRECTION ( 'NONE',  ( -0.000000000000000000, -0.000000000000000000, -1.000000000000000000 ) ) ;
#71671=DIRECTION ( 'NONE',  ( 8.090853898039828715E-17, -9.269810975720166919E-17, 1.000000000000000000 ) ) ;
#71672=DIRECTION ( 'NONE',  ( -0.000000000000000000, -0.000000000000000000, -1.000000000000000000 ) ) ;
#71699=PRODUCT_DEFINITION_CONTEXT ( 'detailed design', #50808, 'design' ) ;
#71715=ORIENTED_EDGE ( 'NONE', *, *, #44849, .T. ) ;
#71801=CIRCLE ( 'NONE', #2211, 11.59999999999999787 ) ;
#72131=CIRCLE ( 'NONE', #16928, 11.59999999999999787 ) ;
#72227=DIRECTION ( 'NONE',  ( -0.000000000000000000, -0.000000000000000000, -1.000000000000000000 ) ) ;
#72249=VECTOR ( 'NONE', #66765, 1000.000000000000000 ) ;
#72255=VECTOR ( 'NONE', #71659, 1000.000000000000000 ) ;
#72295=AXIS2_PLACEMENT_3D ( 'NONE', #68574, #3946, #73816 ) ;
#72296=ORIENTED_EDGE ( 'NONE', *, *, #1764, .T. ) ;
#72303=VERTEX_POINT ( 'NONE', #24708 ) ;
#72473=ORIENTED_EDGE ( 'NONE', *, *, #2882, .F. ) ;
#72532=ADVANCED_FACE ( 'NONE', ( #62653 ), #44977, .T. ) ;
#72596=AXIS2_PLACEMENT_3D ( 'NONE', #54377, #65301, #26161 ) ;
#72690=CYLINDRICAL_SURFACE ( 'NONE', #72295, 12.49999999999999645 ) ;
#72704=DIRECTION ( 'NONE',  ( 8.090853898039828715E-17, -9.269810975720166919E-17, 1.000000000000000000 ) ) ;
#72746=ORIENTED_EDGE ( 'NONE', *, *, #53002, .F. ) ;
#72826=CARTESIAN_POINT ( 'NONE',  ( -8.637688417678527131, 13.69818742750669394, 42.00000000000001421 ) ) ;
#72837=ORIENTED_EDGE ( 'NONE', *, *, #10807, .F. ) ;
#72856=ORIENTED_EDGE ( 'NONE', *, *, #50061, .T. ) ;
#72900=DIRECTION ( 'NONE',  ( 0.000000000000000000, 0.000000000000000000, 1.000000000000000000 ) ) ;
#72915=CIRCLE ( 'NONE', #64579, 12.49999999999999645 ) ;
#72976=VECTOR ( 'NONE', #50287, 1000.000000000000000 ) ;
#72979=AXIS2_PLACEMENT_3D ( 'NONE', #11776, #51271, #62584 ) ;
#72997=CIRCLE ( 'NONE', #22706, 11.59999999999999787 ) ;
#73054=CARTESIAN_POINT ( 'NONE',  ( -12.40464318976454727, 10.41032311384371845, -55.00000000000000000 ) ) ;
#73102=DIRECTION ( 'NONE',  ( 0.000000000000000000, 0.000000000000000000, 1.000000000000000000 ) ) ;
#73129=ADVANCED_FACE ( 'NONE', ( #45277 ), #28327, .T. ) ;
#73172=LINE ( 'NONE', #56269, #15041 ) ;
#73211=AXIS2_PLACEMENT_3D ( 'NONE', #19805, #3299, #49497 ) ;
#73217=CARTESIAN_POINT ( 'NONE',  ( -5.565113727472255967, 10.17789316117534248, -44.99999999999998579 ) ) ;
#73266=DIRECTION ( 'NONE',  ( -0.000000000000000000, -0.000000000000000000, -1.000000000000000000 ) ) ;
#73356=EDGE_LOOP ( 'NONE', ( #72837, #72746 ) ) ;
#73358=VECTOR ( 'NONE', #72704, 1000.000000000000000 ) ;
#73370=CARTESIAN_POINT ( 'NONE',  ( 0.000000000000000000, 0.000000000000000000, 52.00000000000002132 ) ) ;
#73380=ORIENTED_EDGE ( 'NONE', *, *, #53884, .T. ) ;
#73401=PRODUCT ( 'Input Shaft', 'Input Shaft', '', ( #18495 ) ) ;
#73471=AXIS2_PLACEMENT_3D ( 'NONE', #4223, #33888, #67734 ) ;
#73621=LINE ( 'NONE', #45454, #14860 ) ;
#73663=PLANE ( 'NONE',  #30725 ) ;
#73677=VERTEX_POINT ( 'NONE', #2592 ) ;
#73816=DIRECTION ( 'NONE',  ( -1.000000000000000000, 0.000000000000000000, 0.000000000000000000 ) ) ;
#73944=DIRECTION ( 'NONE',  ( 1.000000000000000000, 0.000000000000000000, 0.000000000000000000 ) ) ;
#73957=ORIENTED_EDGE ( 'NONE', *, *, #19463, .F. ) ;
#74018=EDGE_CURVE ( 'NONE', #50553, #42920, #63404, .T. ) ;
#74043=DIRECTION ( 'NONE',  ( 1.000000000000000000, 0.000000000000000000, 0.000000000000000000 ) ) ;
#74047=ORIENTED_EDGE ( 'NONE', *, *, #29369, .F. ) ;
ENDSEC;
END-ISO-10303-21;
